ISO-10303-21;
HEADER;
FILE_DESCRIPTION (('STEP AP203'),
    '1' );
FILE_NAME ('Cleco, Fastener, Shell.step',
    '2026-10-09T13:45:32',
    ( '' ),
    ( '' ),
    'SwSTEP 2.0',
    'SolidWorks 2024',
    '' );
FILE_SCHEMA (( 'AUTOMOTIVE_DESIGN' ));
ENDSEC;

DATA;
#21=EDGE_CURVE ( 'NONE', #2327, #24, #2891, .T. ) ;
#24=VERTEX_POINT ( 'NONE', #7323 ) ;
#34=VECTOR ( 'NONE', #5125, 39.37007874015748143 ) ;
#41=CARTESIAN_POINT ( 'NONE',  ( 0.000000000000000000, 0.6124999999999999334, 0.000000000000000000 ) ) ;
#43=VECTOR ( 'NONE', #928, 39.37007874015748143 ) ;
#47=CARTESIAN_POINT ( 'NONE',  ( 0.000000000000000000, 0.6124999999999999334, 0.000000000000000000 ) ) ;
#66=FACE_OUTER_BOUND ( 'NONE', #5233, .T. ) ;
#69=EDGE_CURVE ( 'NONE', #6638, #4615, #2677, .T. ) ;
#71=ORIENTED_EDGE ( 'NONE', *, *, #7527, .T. ) ;
#73=CIRCLE ( 'NONE', #5578, 0.2425000000000000211 ) ;
#77=DIRECTION ( 'NONE',  ( -1.000000000000000000, 0.000000000000000000, 0.000000000000000000 ) ) ;
#82=EDGE_CURVE ( 'NONE', #7062, #4072, #1053, .T. ) ;
#88=AXIS2_PLACEMENT_3D ( 'NONE', #2138, #3280, #7015 ) ;
#95=DIRECTION ( 'NONE',  ( 0.000000000000000000, 1.000000000000000000, 0.000000000000000000 ) ) ;
#119=DIRECTION ( 'NONE',  ( 0.000000000000000000, 0.000000000000000000, -1.000000000000000000 ) ) ;
#125=EDGE_CURVE ( 'NONE', #2487, #1575, #5560, .T. ) ;
#128=DIRECTION ( 'NONE',  ( -0.000000000000000000, 1.000000000000000000, -0.000000000000000000 ) ) ;
#129=ORIENTED_EDGE ( 'NONE', *, *, #6348, .F. ) ;
#133=EDGE_CURVE ( 'NONE', #2990, #3476, #3761, .T. ) ;
#135=DIRECTION ( 'NONE',  ( 1.000000000000000000, 0.000000000000000000, 0.000000000000000000 ) ) ;
#148=CARTESIAN_POINT ( 'NONE',  ( -0.1250000000000000000, 0.5625000000000000000, 0.03125000000000000000 ) ) ;
#153=DIRECTION ( 'NONE',  ( -0.000000000000000000, -1.000000000000000000, -0.000000000000000000 ) ) ;
#165=CARTESIAN_POINT ( 'NONE',  ( 0.000000000000000000, 1.112500000000000044, 0.2112499999999999933 ) ) ;
#171=CARTESIAN_POINT ( 'NONE',  ( -0.1054677083281892608, 0.6124999999999999334, 0.03125000000000000000 ) ) ;
#173=DIRECTION ( 'NONE',  ( -0.000000000000000000, -0.000000000000000000, -1.000000000000000000 ) ) ;
#180=ORIENTED_EDGE ( 'NONE', *, *, #3278, .F. ) ;
#186=LINE ( 'NONE', #1255, #214 ) ;
#198=DIRECTION ( 'NONE',  ( 0.000000000000000000, 0.000000000000000000, -1.000000000000000000 ) ) ;
#203=AXIS2_PLACEMENT_3D ( 'NONE', #6124, #1765, #1112 ) ;
#204=DIRECTION ( 'NONE',  ( 0.000000000000000000, 1.000000000000000000, 0.000000000000000000 ) ) ;
#214=VECTOR ( 'NONE', #2035, 39.37007874015748143 ) ;
#217=DIRECTION ( 'NONE',  ( -0.000000000000000000, -1.000000000000000000, -0.000000000000000000 ) ) ;
#229=CARTESIAN_POINT ( 'NONE',  ( 0.000000000000000000, 0.6124999999999999334, 0.000000000000000000 ) ) ;
#242=DIRECTION ( 'NONE',  ( -0.000000000000000000, -1.000000000000000000, -0.000000000000000000 ) ) ;
#246=LINE ( 'NONE', #7853, #7674 ) ;
#257=CARTESIAN_POINT ( 'NONE',  ( 0.000000000000000000, 0.03125000000000000000, 0.000000000000000000 ) ) ;
#263=EDGE_LOOP ( 'NONE', ( #2370, #5104, #2202, #5817, #4197, #6775 ) ) ;
#264=ORIENTED_EDGE ( 'NONE', *, *, #6391, .T. ) ;
#288=CARTESIAN_POINT ( 'NONE',  ( 0.000000000000000000, 0.000000000000000000, 0.000000000000000000 ) ) ;
#305=VERTEX_POINT ( 'NONE', #7109 ) ;
#307=CARTESIAN_POINT ( 'NONE',  ( 1.347111479062088626E-17, 0.6124999999999999334, -0.1100000000000000006 ) ) ;
#329=EDGE_CURVE ( 'NONE', #6037, #2842, #7011, .T. ) ;
#344=CIRCLE ( 'NONE', #5453, 0.1100000000000000006 ) ;
#347=DIRECTION ( 'NONE',  ( -0.000000000000000000, -1.000000000000000000, -0.000000000000000000 ) ) ;
#348=CARTESIAN_POINT ( 'NONE',  ( -0.1250000000000000000, 0.5625000000000000000, -0.03125000000000000000 ) ) ;
#353=VERTEX_POINT ( 'NONE', #6414 ) ;
#360=CARTESIAN_POINT ( 'NONE',  ( 1.821662113731687560E-17, 0.03125000000000000000, 0.1487499999999999933 ) ) ;
#366=DIRECTION ( 'NONE',  ( 0.000000000000000000, 1.000000000000000000, 0.000000000000000000 ) ) ;
#367=DIRECTION ( 'NONE',  ( 0.000000000000000000, 1.000000000000000000, 0.000000000000000000 ) ) ;
#384=CYLINDRICAL_SURFACE ( 'NONE', #1117, 0.1799999999999999933 ) ;
#388=ORIENTED_EDGE ( 'NONE', *, *, #6945, .T. ) ;
#394=CARTESIAN_POINT ( 'NONE',  ( 0.000000000000000000, 1.081250000000000044, -0.2112499999999999933 ) ) ;
#395=FACE_OUTER_BOUND ( 'NONE', #5929, .T. ) ;
#398=PLANE ( 'NONE',  #7750 ) ;
#409=VERTEX_POINT ( 'NONE', #2851 ) ;
#430=DIRECTION ( 'NONE',  ( 0.000000000000000000, 0.000000000000000000, -1.000000000000000000 ) ) ;
#434=ORIENTED_EDGE ( 'NONE', *, *, #2573, .T. ) ;
#439=AXIS2_PLACEMENT_3D ( 'NONE', #1148, #5619, #7534 ) ;
#447=CARTESIAN_POINT ( 'NONE',  ( 2.013013176098461537E-17, 0.000000000000000000, 0.1487499999999999933 ) ) ;
#458=ORIENTED_EDGE ( 'NONE', *, *, #3788, .T. ) ;
#460=AXIS2_PLACEMENT_3D ( 'NONE', #1047, #3541, #2921 ) ;
#477=VERTEX_POINT ( 'NONE', #4119 ) ;
#479=AXIS2_PLACEMENT_3D ( 'NONE', #2095, #6484, #870 ) ;
#483=ADVANCED_FACE ( 'NONE', ( #7869 ), #3390, .T. ) ;
#484=CIRCLE ( 'NONE', #7425, 0.1250000000000000000 ) ;
#488=ADVANCED_FACE ( 'NONE', ( #5318 ), #8044, .T. ) ;
#489=CARTESIAN_POINT ( 'NONE',  ( -0.1250000000000000000, 0.6250000000000000000, 0.03125000000000000000 ) ) ;
#492=DIRECTION ( 'NONE',  ( -0.000000000000000000, -1.000000000000000000, -0.000000000000000000 ) ) ;
#513=CARTESIAN_POINT ( 'NONE',  ( 0.000000000000000000, 1.362500000000000044, 0.1250000000000000000 ) ) ;
#514=DIRECTION ( 'NONE',  ( 0.000000000000000000, -1.000000000000000000, 0.000000000000000000 ) ) ;
#521=ADVANCED_FACE ( 'NONE', ( #6580 ), #384, .T. ) ;
#522=EDGE_CURVE ( 'NONE', #3956, #2990, #4520, .T. ) ;
#525=FACE_OUTER_BOUND ( 'NONE', #948, .T. ) ;
#526=VERTEX_POINT ( 'NONE', #3046 ) ;
#533=CARTESIAN_POINT ( 'NONE',  ( -0.1054677083281892608, 0.5625000000000000000, 0.03125000000000000000 ) ) ;
#535=ORIENTED_EDGE ( 'NONE', *, *, #2466, .T. ) ;
#539=DIRECTION ( 'NONE',  ( 0.000000000000000000, 1.000000000000000000, 0.000000000000000000 ) ) ;
#544=CARTESIAN_POINT ( 'NONE',  ( 0.000000000000000000, 0.6124999999999999334, 0.03125000000000000000 ) ) ;
#546=PLANE ( 'NONE',  #710 ) ;
#548=DIRECTION ( 'NONE',  ( -0.000000000000000000, -0.000000000000000000, -1.000000000000000000 ) ) ;
#566=CARTESIAN_POINT ( 'NONE',  ( 1.347111479062088626E-17, 0.000000000000000000, -0.1100000000000000006 ) ) ;
#568=ORIENTED_EDGE ( 'NONE', *, *, #1673, .F. ) ;
#589=ORIENTED_EDGE ( 'NONE', *, *, #2671, .T. ) ;
#594=DIRECTION ( 'NONE',  ( 0.000000000000000000, 1.000000000000000000, 0.000000000000000000 ) ) ;
#601=ORIENTED_EDGE ( 'NONE', *, *, #1330, .T. ) ;
#612=CIRCLE ( 'NONE', #479, 0.1487499999999999933 ) ;
#630=FACE_OUTER_BOUND ( 'NONE', #3426, .T. ) ;
#644=ORIENTED_EDGE ( 'NONE', *, *, #2466, .F. ) ;
#661=VERTEX_POINT ( 'NONE', #5057 ) ;
#665=DIRECTION ( 'NONE',  ( 0.000000000000000000, 0.000000000000000000, 1.000000000000000000 ) ) ;
#669=EDGE_CURVE ( 'NONE', #1476, #3995, #4406, .T. ) ;
#679=EDGE_CURVE ( 'NONE', #4615, #6638, #5834, .T. ) ;
#685=AXIS2_PLACEMENT_3D ( 'NONE', #394, #3596, #4129 ) ;
#687=DIRECTION ( 'NONE',  ( 0.000000000000000000, 0.000000000000000000, 1.000000000000000000 ) ) ;
#691=EDGE_CURVE ( 'NONE', #1756, #1913, #1003, .T. ) ;
#697=CARTESIAN_POINT ( 'NONE',  ( -0.1210307295689817680, 0.6250000000000000000, 0.03125000000000000000 ) ) ;
#710=AXIS2_PLACEMENT_3D ( 'NONE', #8082, #7358, #6820 ) ;
#718=VECTOR ( 'NONE', #514, 39.37007874015748143 ) ;
#724=ORIENTED_EDGE ( 'NONE', *, *, #7926, .F. ) ;
#726=DIRECTION ( 'NONE',  ( 0.000000000000000000, 0.000000000000000000, 1.000000000000000000 ) ) ;
#727=DIRECTION ( 'NONE',  ( -0.000000000000000000, -1.000000000000000000, -0.000000000000000000 ) ) ;
#728=EDGE_CURVE ( 'NONE', #6037, #2029, #73, .T. ) ;
#750=CARTESIAN_POINT ( 'NONE',  ( 0.000000000000000000, 0.6124999999999999334, 0.000000000000000000 ) ) ;
#752=AXIS2_PLACEMENT_3D ( 'NONE', #6453, #5459, #2909 ) ;
#768=DIRECTION ( 'NONE',  ( -1.000000000000000000, 0.000000000000000000, -0.000000000000000000 ) ) ;
#772=DIRECTION ( 'NONE',  ( 0.000000000000000000, 0.000000000000000000, 1.000000000000000000 ) ) ;
#790=CARTESIAN_POINT ( 'NONE',  ( 1.347111479062088626E-17, 1.362500000000000044, -0.1100000000000000006 ) ) ;
#791=CARTESIAN_POINT ( 'NONE',  ( -0.1250000000000000000, 0.5625000000000000000, -0.03125000000000000000 ) ) ;
#828=CIRCLE ( 'NONE', #439, 0.1487499999999999933 ) ;
#836=LINE ( 'NONE', #3530, #1540 ) ;
#840=EDGE_LOOP ( 'NONE', ( #3164, #71, #3687 ) ) ;
#847=CARTESIAN_POINT ( 'NONE',  ( 0.000000000000000000, 1.362500000000000044, 0.000000000000000000 ) ) ;
#848=ORIENTED_EDGE ( 'NONE', *, *, #4685, .T. ) ;
#852=VECTOR ( 'NONE', #204, 39.37007874015748143 ) ;
#857=EDGE_CURVE ( 'NONE', #1913, #7141, #6490, .T. ) ;
#864=AXIS2_PLACEMENT_3D ( 'NONE', #2591, #6363, #5714 ) ;
#867=AXIS2_PLACEMENT_3D ( 'NONE', #41, #2540, #7545 ) ;
#870=DIRECTION ( 'NONE',  ( 0.000000000000000000, 0.000000000000000000, -1.000000000000000000 ) ) ;
#876=CARTESIAN_POINT ( 'NONE',  ( -0.1054677083281892608, 0.000000000000000000, 0.03125000000000000000 ) ) ;
#878=CARTESIAN_POINT ( 'NONE',  ( 2.204364238465235822E-17, 1.050000000000000044, 0.1799999999999999933 ) ) ;
#881=ORIENTED_EDGE ( 'NONE', *, *, #7926, .T. ) ;
#885=ORIENTED_EDGE ( 'NONE', *, *, #5348, .F. ) ;
#886=ADVANCED_FACE ( 'NONE', ( #5263 ), #1526, .T. ) ;
#887=DIRECTION ( 'NONE',  ( 0.000000000000000000, -0.000000000000000000, 1.000000000000000000 ) ) ;
#896=CIRCLE ( 'NONE', #1543, 0.1100000000000000006 ) ;
#908=CARTESIAN_POINT ( 'NONE',  ( 1.347111479062088626E-17, 1.425000000000000044, -0.1100000000000000006 ) ) ;
#913=CARTESIAN_POINT ( 'NONE',  ( 0.000000000000000000, 1.081250000000000044, -0.2425000000000000211 ) ) ;
#925=FACE_OUTER_BOUND ( 'NONE', #6036, .T. ) ;
#928=DIRECTION ( 'NONE',  ( -1.000000000000000000, -0.000000000000000000, -0.000000000000000000 ) ) ;
#933=ORIENTED_EDGE ( 'NONE', *, *, #5244, .F. ) ;
#939=ADVANCED_FACE ( 'NONE', ( #1068, #4884 ), #4311, .T. ) ;
#948=EDGE_LOOP ( 'NONE', ( #3804, #3916, #5726, #3982, #2863, #4641 ) ) ;
#953=EDGE_LOOP ( 'NONE', ( #6127, #848, #434, #2227 ) ) ;
#964=( NAMED_UNIT ( * ) SI_UNIT ( $, .STERADIAN. ) SOLID_ANGLE_UNIT ( ) );
#969=CARTESIAN_POINT ( 'NONE',  ( 0.000000000000000000, 1.393749999999999822, 0.000000000000000000 ) ) ;
#970=AXIS2_PLACEMENT_3D ( 'NONE', #5204, #1587, #2168 ) ;
#978=DIRECTION ( 'NONE',  ( 0.000000000000000000, 1.000000000000000000, 0.000000000000000000 ) ) ;
#990=DIRECTION ( 'NONE',  ( 0.000000000000000000, 0.000000000000000000, 1.000000000000000000 ) ) ;
#1003=CIRCLE ( 'NONE', #7916, 0.1100000000000000006 ) ;
#1010=AXIS2_PLACEMENT_3D ( 'NONE', #3202, #6395, #4556 ) ;
#1024=DIRECTION ( 'NONE',  ( 0.000000000000000000, 1.000000000000000000, 0.000000000000000000 ) ) ;
#1028=DIRECTION ( 'NONE',  ( 0.000000000000000000, 1.000000000000000000, 0.000000000000000000 ) ) ;
#1036=CARTESIAN_POINT ( 'NONE',  ( -0.1250000000000000000, 0.5625000000000000000, 0.03125000000000000000 ) ) ;
#1042=ORIENTED_EDGE ( 'NONE', *, *, #6457, .T. ) ;
#1047=CARTESIAN_POINT ( 'NONE',  ( 0.000000000000000000, 0.6124999999999999334, 0.000000000000000000 ) ) ;
#1053=LINE ( 'NONE', #3546, #1766 ) ;
#1055=DIRECTION ( 'NONE',  ( 0.000000000000000000, 0.000000000000000000, 1.000000000000000000 ) ) ;
#1059=DIRECTION ( 'NONE',  ( 0.000000000000000000, 0.000000000000000000, 1.000000000000000000 ) ) ;
#1063=CARTESIAN_POINT ( 'NONE',  ( 0.1054677083281892608, 0.6124999999999999334, 0.03125000000000000000 ) ) ;
#1066=ORIENTED_EDGE ( 'NONE', *, *, #329, .T. ) ;
#1068=FACE_OUTER_BOUND ( 'NONE', #7114, .T. ) ;
#1074=CARTESIAN_POINT ( 'NONE',  ( 0.1054677083281892608, 0.5625000000000000000, -0.03125000000000000000 ) ) ;
#1095=CARTESIAN_POINT ( 'NONE',  ( 0.000000000000000000, 1.393749999999999822, 0.000000000000000000 ) ) ;
#1110=VERTEX_POINT ( 'NONE', #4397 ) ;
#1112=DIRECTION ( 'NONE',  ( 0.000000000000000000, 0.000000000000000000, -1.000000000000000000 ) ) ;
#1113=VECTOR ( 'NONE', #7817, 39.37007874015748143 ) ;
#1116=VERTEX_POINT ( 'NONE', #2050 ) ;
#1117=AXIS2_PLACEMENT_3D ( 'NONE', #3460, #5967, #7836 ) ;
#1118=AXIS2_PLACEMENT_3D ( 'NONE', #3683, #1917, #6183 ) ;
#1119=CARTESIAN_POINT ( 'NONE',  ( 0.000000000000000000, 1.362500000000000044, 0.1100000000000000006 ) ) ;
#1121=ORIENTED_EDGE ( 'NONE', *, *, #5895, .F. ) ;
#1122=CARTESIAN_POINT ( 'NONE',  ( 0.000000000000000000, 1.081250000000000044, 0.000000000000000000 ) ) ;
#1142=AXIS2_PLACEMENT_3D ( 'NONE', #7646, #5147, #7040 ) ;
#1148=CARTESIAN_POINT ( 'NONE',  ( 0.000000000000000000, 1.425000000000000044, 0.000000000000000000 ) ) ;
#1150=DIRECTION ( 'NONE',  ( 0.000000000000000000, 0.000000000000000000, 1.000000000000000000 ) ) ;
#1154=FACE_OUTER_BOUND ( 'NONE', #3679, .T. ) ;
#1156=ORIENTED_EDGE ( 'NONE', *, *, #7699, .F. ) ;
#1158=ORIENTED_EDGE ( 'NONE', *, *, #6192, .F. ) ;
#1175=CYLINDRICAL_SURFACE ( 'NONE', #1118, 0.1250000000000000000 ) ;
#1177=PLANE ( 'NONE',  #5328 ) ;
#1184=EDGE_CURVE ( 'NONE', #661, #1476, #1914, .T. ) ;
#1223=EDGE_CURVE ( 'NONE', #2029, #6549, #4804, .T. ) ;
#1236=EDGE_CURVE ( 'NONE', #4072, #7994, #246, .T. ) ;
#1243=CIRCLE ( 'NONE', #5048, 0.1799999999999999933 ) ;
#1252=VERTEX_POINT ( 'NONE', #3409 ) ;
#1255=CARTESIAN_POINT ( 'NONE',  ( 0.000000000000000000, 0.000000000000000000, 0.1100000000000000006 ) ) ;
#1273=EDGE_CURVE ( 'NONE', #2327, #1856, #3223, .T. ) ;
#1276=CIRCLE ( 'NONE', #6643, 0.1799999999999999933 ) ;
#1304=CARTESIAN_POINT ( 'NONE',  ( 0.000000000000000000, 0.6124999999999999334, 0.000000000000000000 ) ) ;
#1330=EDGE_CURVE ( 'NONE', #7840, #3971, #2866, .T. ) ;
#1331=DIRECTION ( 'NONE',  ( 0.000000000000000000, 1.000000000000000000, 0.000000000000000000 ) ) ;
#1335=DIRECTION ( 'NONE',  ( -0.000000000000000000, -1.000000000000000000, -0.000000000000000000 ) ) ;
#1355=CARTESIAN_POINT ( 'NONE',  ( 1.530808498934191201E-17, 0.6124999999999999334, -0.1250000000000000000 ) ) ;
#1364=ORIENTED_EDGE ( 'NONE', *, *, #1935, .T. ) ;
#1367=ADVANCED_FACE ( 'NONE', ( #7294 ), #1177, .T. ) ;
#1373=CARTESIAN_POINT ( 'NONE',  ( 0.000000000000000000, 0.6250000000000000000, 0.000000000000000000 ) ) ;
#1375=LINE ( 'NONE', #148, #2506 ) ;
#1388=AXIS2_PLACEMENT_3D ( 'NONE', #2599, #5650, #5106 ) ;
#1390=CIRCLE ( 'NONE', #5983, 0.1250000000000000000 ) ;
#1393=CARTESIAN_POINT ( 'NONE',  ( 0.000000000000000000, 0.000000000000000000, -0.1487499999999999933 ) ) ;
#1400=CIRCLE ( 'NONE', #4293, 0.1799999999999999933 ) ;
#1402=EDGE_LOOP ( 'NONE', ( #4754, #2737, #7775, #2210 ) ) ;
#1420=ADVANCED_FACE ( 'NONE', ( #8012 ), #5570, .F. ) ;
#1425=DIRECTION ( 'NONE',  ( -0.000000000000000000, -1.000000000000000000, -0.000000000000000000 ) ) ;
#1429=ADVANCED_FACE ( 'NONE', ( #525 ), #4302, .T. ) ;
#1430=DIRECTION ( 'NONE',  ( -3.552713678800500929E-15, 0.000000000000000000, 1.000000000000000000 ) ) ;
#1436=ORIENTED_EDGE ( 'NONE', *, *, #679, .F. ) ;
#1451=PLANE ( 'NONE',  #4502 ) ;
#1459=CIRCLE ( 'NONE', #6055, 0.2112499999999999933 ) ;
#1476=VERTEX_POINT ( 'NONE', #1711 ) ;
#1489=DIRECTION ( 'NONE',  ( -0.000000000000000000, -1.000000000000000000, -0.000000000000000000 ) ) ;
#1518=VECTOR ( 'NONE', #1059, 39.37007874015748143 ) ;
#1526=PLANE ( 'NONE',  #6757 ) ;
#1527=ADVANCED_FACE ( 'NONE', ( #3523 ), #398, .F. ) ;
#1536=EDGE_CURVE ( 'NONE', #1856, #409, #1920, .T. ) ;
#1540=VECTOR ( 'NONE', #4188, 39.37007874015748143 ) ;
#1542=ORIENTED_EDGE ( 'NONE', *, *, #7527, .F. ) ;
#1543=AXIS2_PLACEMENT_3D ( 'NONE', #4921, #4270, #6119 ) ;
#1549=DESIGN_CONTEXT ( 'detailed design', #6566, 'design' ) ;
#1555=VERTEX_POINT ( 'NONE', #6832 ) ;
#1560=DIRECTION ( 'NONE',  ( 0.000000000000000000, 0.000000000000000000, -1.000000000000000000 ) ) ;
#1568=ORIENTED_EDGE ( 'NONE', *, *, #2612, .T. ) ;
#1571=CARTESIAN_POINT ( 'NONE',  ( 0.000000000000000000, 1.081250000000000044, 0.000000000000000000 ) ) ;
#1575=VERTEX_POINT ( 'NONE', #4990 ) ;
#1582=DIRECTION ( 'NONE',  ( 0.000000000000000000, -0.000000000000000000, 1.000000000000000000 ) ) ;
#1585=DIRECTION ( 'NONE',  ( -0.000000000000000000, 1.000000000000000000, -0.000000000000000000 ) ) ;
#1587=DIRECTION ( 'NONE',  ( -0.000000000000000000, -1.000000000000000000, -0.000000000000000000 ) ) ;
#1608=ORIENTED_EDGE ( 'NONE', *, *, #4738, .F. ) ;
#1610=DIRECTION ( 'NONE',  ( 0.000000000000000000, 0.000000000000000000, 1.000000000000000000 ) ) ;
#1615=ORIENTED_EDGE ( 'NONE', *, *, #7985, .F. ) ;
#1624=EDGE_CURVE ( 'NONE', #7141, #7062, #1375, .T. ) ;
#1640=ORIENTED_EDGE ( 'NONE', *, *, #329, .F. ) ;
#1646=VECTOR ( 'NONE', #3895, 39.37007874015748143 ) ;
#1661=CIRCLE ( 'NONE', #6375, 0.1250000000000000000 ) ;
#1662=ORIENTED_EDGE ( 'NONE', *, *, #82, .T. ) ;
#1673=EDGE_CURVE ( 'NONE', #6544, #6217, #4609, .T. ) ;
#1684=VERTEX_POINT ( 'NONE', #3963 ) ;
#1688=DIRECTION ( 'NONE',  ( -0.000000000000000000, -1.000000000000000000, -0.000000000000000000 ) ) ;
#1694=LINE ( 'NONE', #4198, #2268 ) ;
#1698=ORIENTED_EDGE ( 'NONE', *, *, #7985, .T. ) ;
#1711=CARTESIAN_POINT ( 'NONE',  ( 0.000000000000000000, 0.6124999999999999334, 0.1250000000000000000 ) ) ;
#1714=PLANE ( 'NONE',  #3573 ) ;
#1724=EDGE_CURVE ( 'NONE', #6311, #6574, #7728, .T. ) ;
#1726=( GEOMETRIC_REPRESENTATION_CONTEXT ( 3 ) GLOBAL_UNCERTAINTY_ASSIGNED_CONTEXT ( ( #6220 ) ) GLOBAL_UNIT_ASSIGNED_CONTEXT ( ( #2225, #5922, #964 ) ) REPRESENTATION_CONTEXT ( 'NONE', 'WORKASPACE' ) );
#1737=AXIS2_PLACEMENT_3D ( 'NONE', #4102, #5912, #6026 ) ;
#1755=CARTESIAN_POINT ( 'NONE',  ( -0.1250000000000000000, 0.5625000000000000000, 0.03125000000000000000 ) ) ;
#1756=VERTEX_POINT ( 'NONE', #2167 ) ;
#1757=EDGE_LOOP ( 'NONE', ( #1640, #5600, #2195, #3060 ) ) ;
#1761=DIRECTION ( 'NONE',  ( -0.000000000000000000, -1.000000000000000000, -0.000000000000000000 ) ) ;
#1764=DIRECTION ( 'NONE',  ( 0.000000000000000000, -1.000000000000000000, -0.000000000000000000 ) ) ;
#1765=DIRECTION ( 'NONE',  ( 0.000000000000000000, -1.000000000000000000, -0.000000000000000000 ) ) ;
#1766=VECTOR ( 'NONE', #6054, 39.37007874015748143 ) ;
#1774=FACE_OUTER_BOUND ( 'NONE', #4349, .T. ) ;
#1782=LINE ( 'NONE', #4251, #6641 ) ;
#1784=EDGE_CURVE ( 'NONE', #6037, #3726, #7871, .T. ) ;
#1795=ADVANCED_FACE ( 'NONE', ( #6667 ), #5664, .T. ) ;
#1798=FACE_OUTER_BOUND ( 'NONE', #3350, .T. ) ;
#1805=VECTOR ( 'NONE', #7718, 39.37007874015748143 ) ;
#1816=LINE ( 'NONE', #6691, #2658 ) ;
#1829=EDGE_CURVE ( 'NONE', #3995, #1575, #5480, .T. ) ;
#1831=ORIENTED_EDGE ( 'NONE', *, *, #6391, .F. ) ;
#1851=FACE_OUTER_BOUND ( 'NONE', #1757, .T. ) ;
#1856=VERTEX_POINT ( 'NONE', #7285 ) ;
#1866=LINE ( 'NONE', #1355, #34 ) ;
#1901=DIRECTION ( 'NONE',  ( -0.000000000000000000, 1.000000000000000000, -0.000000000000000000 ) ) ;
#1913=VERTEX_POINT ( 'NONE', #171 ) ;
#1914=CIRCLE ( 'NONE', #867, 0.1250000000000000000 ) ;
#1916=AXIS2_PLACEMENT_3D ( 'NONE', #2695, #77, #772 ) ;
#1917=DIRECTION ( 'NONE',  ( -0.000000000000000000, 1.000000000000000000, -0.000000000000000000 ) ) ;
#1920=LINE ( 'NONE', #3152, #6581 ) ;
#1924=EDGE_CURVE ( 'NONE', #2842, #7766, #1459, .T. ) ;
#1934=CARTESIAN_POINT ( 'NONE',  ( 0.000000000000000000, 1.393749999999999822, -0.1799999999999999933 ) ) ;
#1935=EDGE_CURVE ( 'NONE', #305, #4615, #1866, .T. ) ;
#1939=DIRECTION ( 'NONE',  ( 0.000000000000000000, -0.000000000000000000, 1.000000000000000000 ) ) ;
#1953=CARTESIAN_POINT ( 'NONE',  ( 0.000000000000000000, 1.393749999999999822, 0.000000000000000000 ) ) ;
#1954=CARTESIAN_POINT ( 'NONE',  ( 0.000000000000000000, 1.081250000000000044, 0.2112499999999999933 ) ) ;
#1961=ORIENTED_EDGE ( 'NONE', *, *, #4243, .F. ) ;
#1972=CARTESIAN_POINT ( 'NONE',  ( -0.1250000000000000000, 0.6250000000000000000, -0.03125000000000000000 ) ) ;
#1988=LINE ( 'NONE', #2034, #5551 ) ;
#1993=FACE_OUTER_BOUND ( 'NONE', #263, .T. ) ;
#1996=CARTESIAN_POINT ( 'NONE',  ( 0.1250000000000000000, 0.5625000000000000000, 0.03125000000000000000 ) ) ;
#1998=ORIENTED_EDGE ( 'NONE', *, *, #4733, .T. ) ;
#1999=CIRCLE ( 'NONE', #5141, 0.03125000000000000694 ) ;
#2005=CARTESIAN_POINT ( 'NONE',  ( 0.000000000000000000, 1.050000000000000044, 0.000000000000000000 ) ) ;
#2018=LINE ( 'NONE', #1972, #5124 ) ;
#2027=ADVANCED_FACE ( 'NONE', ( #925 ), #2914, .T. ) ;
#2029=VERTEX_POINT ( 'NONE', #2912 ) ;
#2034=CARTESIAN_POINT ( 'NONE',  ( 1.347111479062088626E-17, 0.000000000000000000, -0.1100000000000000006 ) ) ;
#2035=DIRECTION ( 'NONE',  ( -0.000000000000000000, 1.000000000000000000, -0.000000000000000000 ) ) ;
#2038=EDGE_CURVE ( 'NONE', #7840, #2261, #4191, .T. ) ;
#2050=CARTESIAN_POINT ( 'NONE',  ( 0.1210307295689817542, 0.6124999999999999334, -0.03125000000000000000 ) ) ;
#2052=CIRCLE ( 'NONE', #1388, 0.1487499999999999933 ) ;
#2072=ORIENTED_EDGE ( 'NONE', *, *, #1184, .T. ) ;
#2074=DIRECTION ( 'NONE',  ( 0.000000000000000000, 0.000000000000000000, 1.000000000000000000 ) ) ;
#2075=VERTEX_POINT ( 'NONE', #878 ) ;
#2095=CARTESIAN_POINT ( 'NONE',  ( 0.000000000000000000, 0.000000000000000000, 0.000000000000000000 ) ) ;
#2097=ORIENTED_EDGE ( 'NONE', *, *, #2479, .F. ) ;
#2102=CARTESIAN_POINT ( 'NONE',  ( -1.693368449338919598E-15, 1.112500000000000044, 0.2425000000000000211 ) ) ;
#2138=CARTESIAN_POINT ( 'NONE',  ( 0.000000000000000000, 1.112500000000000044, 0.000000000000000000 ) ) ;
#2162=CARTESIAN_POINT ( 'NONE',  ( -1.256933281983527929E-15, 1.425000000000000044, 0.1799999999999999933 ) ) ;
#2167=CARTESIAN_POINT ( 'NONE',  ( 0.000000000000000000, 0.6124999999999999334, 0.1100000000000000006 ) ) ;
#2168=DIRECTION ( 'NONE',  ( 0.000000000000000000, 0.000000000000000000, -1.000000000000000000 ) ) ;
#2175=CARTESIAN_POINT ( 'NONE',  ( 0.000000000000000000, 1.393749999999999822, 0.000000000000000000 ) ) ;
#2183=ORIENTED_EDGE ( 'NONE', *, *, #1624, .F. ) ;
#2184=AXIS2_PLACEMENT_3D ( 'NONE', #4795, #242, #6184 ) ;
#2193=ADVANCED_FACE ( 'NONE', ( #6247 ), #3128, .T. ) ;
#2194=( LENGTH_UNIT ( ) NAMED_UNIT ( * ) SI_UNIT ( $, .METRE. ) );
#2195=ORIENTED_EDGE ( 'NONE', *, *, #6434, .T. ) ;
#2200=AXIS2_PLACEMENT_3D ( 'NONE', #2674, #2297, #2956 ) ;
#2201=AXIS2_PLACEMENT_3D ( 'NONE', #348, #3539, #7315 ) ;
#2202=ORIENTED_EDGE ( 'NONE', *, *, #4249, .T. ) ;
#2203=EDGE_LOOP ( 'NONE', ( #3418, #180, #6480, #933 ) ) ;
#2209=DIRECTION ( 'NONE',  ( -0.000000000000000000, -1.000000000000000000, -0.000000000000000000 ) ) ;
#2210=ORIENTED_EDGE ( 'NONE', *, *, #2671, .F. ) ;
#2216=CARTESIAN_POINT ( 'NONE',  ( 0.1250000000000000000, 0.6250000000000000000, 0.03125000000000000000 ) ) ;
#2221=DIRECTION ( 'NONE',  ( 0.000000000000000000, -1.000000000000000000, 0.000000000000000000 ) ) ;
#2223=ORIENTED_EDGE ( 'NONE', *, *, #4738, .T. ) ;
#2225=( CONVERSION_BASED_UNIT ( 'INCH', #6575 ) LENGTH_UNIT ( ) NAMED_UNIT ( #6154 ) );
#2227=ORIENTED_EDGE ( 'NONE', *, *, #3028, .F. ) ;
#2245=LINE ( 'NONE', #6561, #4928 ) ;
#2256=AXIS2_PLACEMENT_3D ( 'NONE', #5858, #978, #5810 ) ;
#2261=VERTEX_POINT ( 'NONE', #5778 ) ;
#2268=VECTOR ( 'NONE', #6039, 39.37007874015748143 ) ;
#2270=DIRECTION ( 'NONE',  ( 1.000000000000000000, 0.000000000000000000, 0.000000000000000000 ) ) ;
#2278=FACE_BOUND ( 'NONE', #4220, .T. ) ;
#2280=CIRCLE ( 'NONE', #5430, 0.1250000000000000000 ) ;
#2288=ORIENTED_EDGE ( 'NONE', *, *, #5053, .T. ) ;
#2289=CARTESIAN_POINT ( 'NONE',  ( 0.000000000000000000, 0.5625000000000000000, 0.000000000000000000 ) ) ;
#2297=DIRECTION ( 'NONE',  ( -0.000000000000000000, 1.000000000000000000, -0.000000000000000000 ) ) ;
#2298=SHAPE_REPRESENTATION ( 'Cleco, Fastener, Shell', ( #3555 ), #1726 ) ;
#2318=DIRECTION ( 'NONE',  ( 0.000000000000000000, -0.000000000000000000, 1.000000000000000000 ) ) ;
#2319=CIRCLE ( 'NONE', #4555, 0.2112499999999999933 ) ;
#2326=CIRCLE ( 'NONE', #6911, 0.2112499999999999933 ) ;
#2327=VERTEX_POINT ( 'NONE', #1934 ) ;
#2329=EDGE_CURVE ( 'NONE', #3476, #5356, #7236, .T. ) ;
#2333=DIRECTION ( 'NONE',  ( 0.000000000000000000, 0.000000000000000000, 1.000000000000000000 ) ) ;
#2337=DIRECTION ( 'NONE',  ( -4.440892098500626162E-15, 0.000000000000000000, 1.000000000000000000 ) ) ;
#2370=ORIENTED_EDGE ( 'NONE', *, *, #857, .T. ) ;
#2389=VECTOR ( 'NONE', #3654, 39.37007874015748143 ) ;
#2395=CARTESIAN_POINT ( 'NONE',  ( 0.1210307295689817542, 0.6124999999999999334, 0.03125000000000000000 ) ) ;
#2397=AXIS2_PLACEMENT_3D ( 'NONE', #1122, #539, #7909 ) ;
#2412=VECTOR ( 'NONE', #6140, 39.37007874015748143 ) ;
#2428=CIRCLE ( 'NONE', #2184, 0.2112499999999999933 ) ;
#2444=DIRECTION ( 'NONE',  ( -1.000000000000000000, 0.000000000000000000, 0.000000000000000000 ) ) ;
#2466=EDGE_CURVE ( 'NONE', #4072, #353, #3525, .T. ) ;
#2468=ADVANCED_FACE ( 'NONE', ( #4140 ), #7821, .F. ) ;
#2470=LINE ( 'NONE', #544, #4652 ) ;
#2479=EDGE_CURVE ( 'NONE', #526, #5676, #2786, .T. ) ;
#2485=ORIENTED_EDGE ( 'NONE', *, *, #1829, .T. ) ;
#2487=VERTEX_POINT ( 'NONE', #2216 ) ;
#2498=LINE ( 'NONE', #4969, #7676 ) ;
#2506=VECTOR ( 'NONE', #4334, 39.37007874015748143 ) ;
#2540=DIRECTION ( 'NONE',  ( 0.000000000000000000, 1.000000000000000000, 0.000000000000000000 ) ) ;
#2551=CIRCLE ( 'NONE', #4912, 0.2425000000000000211 ) ;
#2573=EDGE_CURVE ( 'NONE', #6542, #6342, #7244, .T. ) ;
#2580=CARTESIAN_POINT ( 'NONE',  ( 0.000000000000000000, 1.050000000000000044, 0.000000000000000000 ) ) ;
#2588=DIRECTION ( 'NONE',  ( -0.000000000000000000, -1.000000000000000000, -0.000000000000000000 ) ) ;
#2591=CARTESIAN_POINT ( 'NONE',  ( 0.000000000000000000, 1.362500000000000044, 0.000000000000000000 ) ) ;
#2597=FACE_OUTER_BOUND ( 'NONE', #7070, .T. ) ;
#2599=CARTESIAN_POINT ( 'NONE',  ( 0.000000000000000000, 0.000000000000000000, 0.000000000000000000 ) ) ;
#2604=CARTESIAN_POINT ( 'NONE',  ( 0.000000000000000000, 0.6124999999999999334, 0.000000000000000000 ) ) ;
#2606=VERTEX_POINT ( 'NONE', #447 ) ;
#2612=EDGE_CURVE ( 'NONE', #7141, #7994, #4232, .T. ) ;
#2613=DIRECTION ( 'NONE',  ( 0.000000000000000000, 0.000000000000000000, -1.000000000000000000 ) ) ;
#2619=DIRECTION ( 'NONE',  ( 0.000000000000000000, 1.000000000000000000, 0.000000000000000000 ) ) ;
#2621=EDGE_CURVE ( 'NONE', #5902, #477, #3026, .T. ) ;
#2645=AXIS2_PLACEMENT_3D ( 'NONE', #7950, #4277, #6810 ) ;
#2656=DIRECTION ( 'NONE',  ( -0.000000000000000000, -1.000000000000000000, -0.000000000000000000 ) ) ;
#2658=VECTOR ( 'NONE', #3629, 39.37007874015748143 ) ;
#2663=PLANE ( 'NONE',  #4771 ) ;
#2671=EDGE_CURVE ( 'NONE', #1856, #3378, #4492, .T. ) ;
#2674=CARTESIAN_POINT ( 'NONE',  ( 0.000000000000000000, 0.000000000000000000, 0.000000000000000000 ) ) ;
#2677=CIRCLE ( 'NONE', #6613, 0.1250000000000000000 ) ;
#2678=VECTOR ( 'NONE', #6883, 39.37007874015748143 ) ;
#2681=EDGE_LOOP ( 'NONE', ( #5503, #4729, #724 ) ) ;
#2689=CARTESIAN_POINT ( 'NONE',  ( 1.821662113731687560E-17, 1.393749999999999822, -0.1487499999999999933 ) ) ;
#2695=CARTESIAN_POINT ( 'NONE',  ( 0.000000000000000000, 0.03125000000000000000, -0.1487499999999999933 ) ) ;
#2709=ORIENTED_EDGE ( 'NONE', *, *, #7281, .F. ) ;
#2717=LINE ( 'NONE', #5228, #1805 ) ;
#2724=ADVANCED_FACE ( 'NONE', ( #6235 ), #1714, .F. ) ;
#2736=EDGE_CURVE ( 'NONE', #3378, #4578, #828, .T. ) ;
#2737=ORIENTED_EDGE ( 'NONE', *, *, #2887, .T. ) ;
#2745=DIRECTION ( 'NONE',  ( 1.000000000000000000, 0.000000000000000000, 0.000000000000000000 ) ) ;
#2748=DIRECTION ( 'NONE',  ( 0.000000000000000000, 1.000000000000000000, 0.000000000000000000 ) ) ;
#2762=ORIENTED_EDGE ( 'NONE', *, *, #2329, .F. ) ;
#2784=ORIENTED_EDGE ( 'NONE', *, *, #2573, .F. ) ;
#2786=CIRCLE ( 'NONE', #3833, 0.1100000000000000006 ) ;
#2787=ADVANCED_BREP_SHAPE_REPRESENTATION ( '', ( #6340, #3555 ), #1726 ) ;
#2792=AXIS2_PLACEMENT_3D ( 'NONE', #6068, #7941, #2333 ) ;
#2804=ORIENTED_EDGE ( 'NONE', *, *, #5901, .F. ) ;
#2805=DIRECTION ( 'NONE',  ( 0.000000000000000000, 0.000000000000000000, -1.000000000000000000 ) ) ;
#2809=CARTESIAN_POINT ( 'NONE',  ( 0.000000000000000000, 0.000000000000000000, 0.000000000000000000 ) ) ;
#2813=AXIS2_PLACEMENT_3D ( 'NONE', #288, #5871, #4065 ) ;
#2816=FACE_BOUND ( 'NONE', #3524, .T. ) ;
#2817=LINE ( 'NONE', #5975, #3632 ) ;
#2823=CARTESIAN_POINT ( 'NONE',  ( 0.000000000000000000, 1.081250000000000044, 0.000000000000000000 ) ) ;
#2832=FACE_OUTER_BOUND ( 'NONE', #6572, .T. ) ;
#2835=EDGE_LOOP ( 'NONE', ( #1568, #7995, #4048, #2183 ) ) ;
#2842=VERTEX_POINT ( 'NONE', #4463 ) ;
#2848=CARTESIAN_POINT ( 'NONE',  ( -0.1250000000000000000, 0.5625000000000000000, 0.03125000000000000000 ) ) ;
#2851=CARTESIAN_POINT ( 'NONE',  ( 2.204364238465235822E-17, 1.112500000000000044, 0.1799999999999999933 ) ) ;
#2863=ORIENTED_EDGE ( 'NONE', *, *, #522, .T. ) ;
#2864=LINE ( 'NONE', #5939, #1113 ) ;
#2866=LINE ( 'NONE', #7892, #1518 ) ;
#2868=CARTESIAN_POINT ( 'NONE',  ( 0.000000000000000000, 0.000000000000000000, 0.000000000000000000 ) ) ;
#2879=DIRECTION ( 'NONE',  ( -0.000000000000000000, -1.000000000000000000, -0.000000000000000000 ) ) ;
#2883=ADVANCED_FACE ( 'NONE', ( #1993 ), #6386, .T. ) ;
#2887=EDGE_CURVE ( 'NONE', #2327, #4578, #6066, .T. ) ;
#2888=CARTESIAN_POINT ( 'NONE',  ( 0.1250000000000000000, 0.5625000000000000000, 0.03125000000000000000 ) ) ;
#2891=LINE ( 'NONE', #7922, #3469 ) ;
#2899=CARTESIAN_POINT ( 'NONE',  ( 0.000000000000000000, 0.6124999999999999334, 0.000000000000000000 ) ) ;
#2900=EDGE_LOOP ( 'NONE', ( #5351, #3384, #6718, #1542, #644, #7504 ) ) ;
#2901=DIRECTION ( 'NONE',  ( 0.000000000000000000, 1.000000000000000000, 0.000000000000000000 ) ) ;
#2909=DIRECTION ( 'NONE',  ( 0.000000000000000000, 0.000000000000000000, 1.000000000000000000 ) ) ;
#2912=CARTESIAN_POINT ( 'NONE',  ( 2.969768487932331731E-17, 1.081250000000000044, 0.2425000000000000211 ) ) ;
#2914=TOROIDAL_SURFACE ( 'NONE', #3443, 0.2112499999999999933, 0.03125000000000000000 ) ;
#2919=CARTESIAN_POINT ( 'NONE',  ( 0.000000000000000000, 1.112500000000000044, 0.000000000000000000 ) ) ;
#2921=DIRECTION ( 'NONE',  ( 0.000000000000000000, 0.000000000000000000, 1.000000000000000000 ) ) ;
#2925=ADVANCED_FACE ( 'NONE', ( #3404 ), #4667, .T. ) ;
#2936=EDGE_CURVE ( 'NONE', #6542, #2606, #1999, .T. ) ;
#2943=FACE_OUTER_BOUND ( 'NONE', #4650, .T. ) ;
#2947=ORIENTED_EDGE ( 'NONE', *, *, #4450, .F. ) ;
#2948=CARTESIAN_POINT ( 'NONE',  ( -0.1250000000000000000, 0.6250000000000000000, 0.03125000000000000000 ) ) ;
#2956=DIRECTION ( 'NONE',  ( 0.000000000000000000, 0.000000000000000000, 1.000000000000000000 ) ) ;
#2962=ORIENTED_EDGE ( 'NONE', *, *, #5383, .F. ) ;
#2963=AXIS2_PLACEMENT_3D ( 'NONE', #2604, #5111, #6427 ) ;
#2964=CIRCLE ( 'NONE', #88, 0.1799999999999999933 ) ;
#2972=PRODUCT ( 'Cleco, Fastener, Shell', 'Cleco, Fastener, Shell', '', ( #5396 ) ) ;
#2974=CARTESIAN_POINT ( 'NONE',  ( 0.1250000000000000000, 0.5625000000000000000, -0.03125000000000000000 ) ) ;
#2990=VERTEX_POINT ( 'NONE', #7242 ) ;
#2999=ORIENTED_EDGE ( 'NONE', *, *, #6434, .F. ) ;
#3012=DIRECTION ( 'NONE',  ( -1.000000000000000000, 0.000000000000000000, 0.000000000000000000 ) ) ;
#3026=LINE ( 'NONE', #2948, #2389 ) ;
#3028=EDGE_CURVE ( 'NONE', #1555, #6342, #5327, .T. ) ;
#3046=CARTESIAN_POINT ( 'NONE',  ( 0.000000000000000000, 0.000000000000000000, 0.1100000000000000006 ) ) ;
#3060=ORIENTED_EDGE ( 'NONE', *, *, #1924, .F. ) ;
#3063=VECTOR ( 'NONE', #7107, 39.37007874015748143 ) ;
#3078=AXIS2_PLACEMENT_3D ( 'NONE', #2823, #1024, #6062 ) ;
#3095=ORIENTED_EDGE ( 'NONE', *, *, #4943, .F. ) ;
#3096=ORIENTED_EDGE ( 'NONE', *, *, #4249, .F. ) ;
#3106=CIRCLE ( 'NONE', #4286, 0.03125000000000000694 ) ;
#3111=ORIENTED_EDGE ( 'NONE', *, *, #4127, .F. ) ;
#3112=CARTESIAN_POINT ( 'NONE',  ( 0.1250000000000000000, 0.5625000000000000000, -0.03125000000000000000 ) ) ;
#3116=EDGE_LOOP ( 'NONE', ( #7035, #6079, #3328, #885 ) ) ;
#3128=PLANE ( 'NONE',  #2645 ) ;
#3152=CARTESIAN_POINT ( 'NONE',  ( 2.204364238465235822E-17, 0.000000000000000000, 0.1799999999999999933 ) ) ;
#3164=ORIENTED_EDGE ( 'NONE', *, *, #6600, .T. ) ;
#3182=DIRECTION ( 'NONE',  ( 0.000000000000000000, 0.000000000000000000, 1.000000000000000000 ) ) ;
#3194=CIRCLE ( 'NONE', #7773, 0.1487499999999999933 ) ;
#3199=ORIENTED_EDGE ( 'NONE', *, *, #4127, .T. ) ;
#3201=ADVANCED_FACE ( 'NONE', ( #395, #2278 ), #4791, .T. ) ;
#3202=CARTESIAN_POINT ( 'NONE',  ( 2.587066363198783776E-17, 1.081250000000000044, 0.2112499999999999933 ) ) ;
#3211=CARTESIAN_POINT ( 'NONE',  ( 0.000000000000000000, 1.081250000000000044, 0.000000000000000000 ) ) ;
#3216=EDGE_LOOP ( 'NONE', ( #4430, #1698, #3455 ) ) ;
#3223=CIRCLE ( 'NONE', #5058, 0.1799999999999999933 ) ;
#3231=EDGE_CURVE ( 'NONE', #4366, #1756, #3847, .T. ) ;
#3232=ADVANCED_FACE ( 'NONE', ( #7223 ), #6722, .T. ) ;
#3247=DIRECTION ( 'NONE',  ( 0.000000000000000000, 0.000000000000000000, 1.000000000000000000 ) ) ;
#3262=DIRECTION ( 'NONE',  ( -0.000000000000000000, 1.000000000000000000, -0.000000000000000000 ) ) ;
#3267=ORIENTED_EDGE ( 'NONE', *, *, #21, .F. ) ;
#3278=EDGE_CURVE ( 'NONE', #3971, #5356, #7758, .T. ) ;
#3280=DIRECTION ( 'NONE',  ( -0.000000000000000000, -1.000000000000000000, -0.000000000000000000 ) ) ;
#3282=CARTESIAN_POINT ( 'NONE',  ( 0.1054677083281892608, 0.000000000000000000, 0.03125000000000000000 ) ) ;
#3288=ADVANCED_FACE ( 'NONE', ( #3420 ), #7891, .T. ) ;
#3290=ORIENTED_EDGE ( 'NONE', *, *, #5448, .F. ) ;
#3299=ORIENTED_EDGE ( 'NONE', *, *, #691, .T. ) ;
#3309=DIRECTION ( 'NONE',  ( 1.000000000000000000, -0.000000000000000000, 1.224646799147353207E-16 ) ) ;
#3325=LINE ( 'NONE', #6296, #852 ) ;
#3328=ORIENTED_EDGE ( 'NONE', *, *, #21, .T. ) ;
#3334=ORIENTED_EDGE ( 'NONE', *, *, #4243, .T. ) ;
#3337=ORIENTED_EDGE ( 'NONE', *, *, #7796, .T. ) ;
#3339=SHAPE_REPRESENTATION_RELATIONSHIP ( 'NONE' , 'NONE' ,  #2298, #2787 ) ;
#3350=EDGE_LOOP ( 'NONE', ( #1156, #1364, #5284, #4503, #7870, #7939, #7105, #388, #5889 ) ) ;
#3351=ORIENTED_EDGE ( 'NONE', *, *, #69, .T. ) ;
#3352=FACE_OUTER_BOUND ( 'NONE', #7820, .T. ) ;
#3362=AXIS2_PLACEMENT_3D ( 'NONE', #2005, #2588, #2613 ) ;
#3364=DIRECTION ( 'NONE',  ( 8.881784197001252323E-16, 0.000000000000000000, 1.000000000000000000 ) ) ;
#3367=DIRECTION ( 'NONE',  ( -0.000000000000000000, -1.000000000000000000, -0.000000000000000000 ) ) ;
#3370=VECTOR ( 'NONE', #548, 39.37007874015748143 ) ;
#3378=VERTEX_POINT ( 'NONE', #5424 ) ;
#3382=ADVANCED_FACE ( 'NONE', ( #1851 ), #5942, .T. ) ;
#3384=ORIENTED_EDGE ( 'NONE', *, *, #6979, .F. ) ;
#3390=CYLINDRICAL_SURFACE ( 'NONE', #3868, 0.1799999999999999933 ) ;
#3392=ORIENTED_EDGE ( 'NONE', *, *, #3601, .F. ) ;
#3395=EDGE_CURVE ( 'NONE', #1110, #1116, #1694, .T. ) ;
#3398=EDGE_CURVE ( 'NONE', #5902, #661, #1816, .T. ) ;
#3400=CARTESIAN_POINT ( 'NONE',  ( 2.778417425565558062E-17, 1.050000000000000044, 0.2112499999999999933 ) ) ;
#3404=FACE_OUTER_BOUND ( 'NONE', #4793, .T. ) ;
#3409=CARTESIAN_POINT ( 'NONE',  ( -0.1250000000000000000, 0.6250000000000000000, 0.000000000000000000 ) ) ;
#3418=ORIENTED_EDGE ( 'NONE', *, *, #2329, .T. ) ;
#3420=FACE_OUTER_BOUND ( 'NONE', #3608, .T. ) ;
#3424=ORIENTED_EDGE ( 'NONE', *, *, #3788, .F. ) ;
#3426=EDGE_LOOP ( 'NONE', ( #3512, #1436 ) ) ;
#3429=DIRECTION ( 'NONE',  ( -0.000000000000000000, 1.000000000000000000, -0.000000000000000000 ) ) ;
#3443=AXIS2_PLACEMENT_3D ( 'NONE', #6034, #1688, #5381 ) ;
#3453=VECTOR ( 'NONE', #2209, 39.37007874015748143 ) ;
#3455=ORIENTED_EDGE ( 'NONE', *, *, #6328, .F. ) ;
#3460=CARTESIAN_POINT ( 'NONE',  ( 0.000000000000000000, 0.000000000000000000, 0.000000000000000000 ) ) ;
#3469=VECTOR ( 'NONE', #1425, 39.37007874015748143 ) ;
#3476=VERTEX_POINT ( 'NONE', #1074 ) ;
#3478=CARTESIAN_POINT ( 'NONE',  ( 1.530808498934191201E-17, 1.362500000000000044, -0.1250000000000000000 ) ) ;
#3486=EDGE_CURVE ( 'NONE', #4578, #3378, #3194, .T. ) ;
#3499=ADVANCED_FACE ( 'NONE', ( #1774 ), #6362, .F. ) ;
#3500=CIRCLE ( 'NONE', #752, 0.1250000000000000000 ) ;
#3512=ORIENTED_EDGE ( 'NONE', *, *, #69, .F. ) ;
#3515=CARTESIAN_POINT ( 'NONE',  ( 0.000000000000000000, 0.6124999999999999334, 0.1250000000000000000 ) ) ;
#3523=FACE_OUTER_BOUND ( 'NONE', #3216, .T. ) ;
#3524=EDGE_LOOP ( 'NONE', ( #5628, #568 ) ) ;
#3525=LINE ( 'NONE', #7179, #6846 ) ;
#3530=CARTESIAN_POINT ( 'NONE',  ( 0.000000000000000000, 0.6124999999999999334, -0.03125000000000000000 ) ) ;
#3538=CARTESIAN_POINT ( 'NONE',  ( 0.000000000000000000, 0.6124999999999999334, 0.000000000000000000 ) ) ;
#3539=DIRECTION ( 'NONE',  ( 0.000000000000000000, 0.000000000000000000, 1.000000000000000000 ) ) ;
#3541=DIRECTION ( 'NONE',  ( -0.000000000000000000, -1.000000000000000000, -0.000000000000000000 ) ) ;
#3543=DIRECTION ( 'NONE',  ( -0.000000000000000000, -1.000000000000000000, -0.000000000000000000 ) ) ;
#3545=FACE_OUTER_BOUND ( 'NONE', #2681, .T. ) ;
#3546=CARTESIAN_POINT ( 'NONE',  ( -0.1250000000000000000, 0.5625000000000000000, -0.03125000000000000000 ) ) ;
#3551=ORIENTED_EDGE ( 'NONE', *, *, #6513, .F. ) ;
#3555=AXIS2_PLACEMENT_3D ( 'NONE', #5720, #6981, #135 ) ;
#3558=ORIENTED_EDGE ( 'NONE', *, *, #669, .T. ) ;
#3567=AXIS2_PLACEMENT_3D ( 'NONE', #6892, #2656, #1430 ) ;
#3573=AXIS2_PLACEMENT_3D ( 'NONE', #3689, #4221, #7894 ) ;
#3584=AXIS2_PLACEMENT_3D ( 'NONE', #5433, #3543, #430 ) ;
#3592=LINE ( 'NONE', #6099, #3370 ) ;
#3596=DIRECTION ( 'NONE',  ( -1.000000000000000000, 0.000000000000000000, 0.000000000000000000 ) ) ;
#3601=EDGE_CURVE ( 'NONE', #5356, #4366, #4443, .T. ) ;
#3608=EDGE_LOOP ( 'NONE', ( #3730, #4958, #3740, #5225 ) ) ;
#3610=AXIS2_PLACEMENT_3D ( 'NONE', #969, #5884, #4163 ) ;
#3617=CARTESIAN_POINT ( 'NONE',  ( -0.1250000000000000000, 0.5625000000000000000, 0.03125000000000000000 ) ) ;
#3629=DIRECTION ( 'NONE',  ( 0.000000000000000000, -1.000000000000000000, 0.000000000000000000 ) ) ;
#3632=VECTOR ( 'NONE', #7238, 39.37007874015748143 ) ;
#3645=ADVANCED_FACE ( 'NONE', ( #630, #3786 ), #2663, .F. ) ;
#3654=DIRECTION ( 'NONE',  ( -1.000000000000000000, -0.000000000000000000, -0.000000000000000000 ) ) ;
#3664=DIRECTION ( 'NONE',  ( 1.000000000000000000, 0.000000000000000000, 0.000000000000000000 ) ) ;
#3675=FACE_OUTER_BOUND ( 'NONE', #5403, .T. ) ;
#3679=EDGE_LOOP ( 'NONE', ( #3957, #7644 ) ) ;
#3683=CARTESIAN_POINT ( 'NONE',  ( 0.000000000000000000, 0.6124999999999999334, 0.000000000000000000 ) ) ;
#3686=DIRECTION ( 'NONE',  ( 0.000000000000000000, -0.000000000000000000, 1.000000000000000000 ) ) ;
#3687=ORIENTED_EDGE ( 'NONE', *, *, #6945, .F. ) ;
#3689=CARTESIAN_POINT ( 'NONE',  ( -0.1250000000000000000, 0.6250000000000000000, 0.03125000000000000000 ) ) ;
#3716=SHAPE_DEFINITION_REPRESENTATION ( #5462, #2298 ) ;
#3726=VERTEX_POINT ( 'NONE', #4457 ) ;
#3730=ORIENTED_EDGE ( 'NONE', *, *, #1223, .F. ) ;
#3739=ADVANCED_FACE ( 'NONE', ( #3352 ), #1451, .T. ) ;
#3740=ORIENTED_EDGE ( 'NONE', *, *, #1784, .T. ) ;
#3749=ORIENTED_EDGE ( 'NONE', *, *, #4450, .T. ) ;
#3753=ORIENTED_EDGE ( 'NONE', *, *, #1784, .F. ) ;
#3761=LINE ( 'NONE', #7405, #718 ) ;
#3765=ORIENTED_EDGE ( 'NONE', *, *, #669, .F. ) ;
#3786=FACE_BOUND ( 'NONE', #5102, .T. ) ;
#3788=EDGE_CURVE ( 'NONE', #7457, #7619, #7255, .T. ) ;
#3798=DIRECTION ( 'NONE',  ( 0.000000000000000000, 1.000000000000000000, 0.000000000000000000 ) ) ;
#3804=ORIENTED_EDGE ( 'NONE', *, *, #4340, .T. ) ;
#3811=ORIENTED_EDGE ( 'NONE', *, *, #4943, .T. ) ;
#3816=EDGE_LOOP ( 'NONE', ( #1961, #7972, #7829, #3551, #7119, #3856, #6187, #2947 ) ) ;
#3817=LINE ( 'NONE', #7614, #3882 ) ;
#3833=AXIS2_PLACEMENT_3D ( 'NONE', #2868, #2901, #990 ) ;
#3835=ADVANCED_FACE ( 'NONE', ( #2597 ), #7118, .F. ) ;
#3843=DIRECTION ( 'NONE',  ( -1.000000000000000000, 0.000000000000000000, 0.000000000000000000 ) ) ;
#3847=CIRCLE ( 'NONE', #6597, 0.1100000000000000006 ) ;
#3856=ORIENTED_EDGE ( 'NONE', *, *, #857, .F. ) ;
#3868=AXIS2_PLACEMENT_3D ( 'NONE', #2809, #4774, #7272 ) ;
#3880=DIRECTION ( 'NONE',  ( -0.000000000000000000, -1.000000000000000000, -0.000000000000000000 ) ) ;
#3882=VECTOR ( 'NONE', #5775, 39.37007874015748143 ) ;
#3895=DIRECTION ( 'NONE',  ( 0.000000000000000000, 1.000000000000000000, 0.000000000000000000 ) ) ;
#3900=APPLICATION_CONTEXT ( 'configuration controlled 3d designs of mechanical parts and assemblies' ) ;
#3909=EDGE_LOOP ( 'NONE', ( #6781, #4716, #5310 ) ) ;
#3916=ORIENTED_EDGE ( 'NONE', *, *, #7699, .T. ) ;
#3956=VERTEX_POINT ( 'NONE', #307 ) ;
#3957=ORIENTED_EDGE ( 'NONE', *, *, #6192, .T. ) ;
#3963=CARTESIAN_POINT ( 'NONE',  ( 0.1250000000000000000, 0.6250000000000000000, 0.000000000000000000 ) ) ;
#3971=VERTEX_POINT ( 'NONE', #2888 ) ;
#3982=ORIENTED_EDGE ( 'NONE', *, *, #5991, .T. ) ;
#3987=AXIS2_PLACEMENT_3D ( 'NONE', #6256, #1901, #665 ) ;
#3995=VERTEX_POINT ( 'NONE', #4052 ) ;
#4006=ORIENTED_EDGE ( 'NONE', *, *, #3278, .T. ) ;
#4037=DIRECTION ( 'NONE',  ( 0.000000000000000000, 1.000000000000000000, 0.000000000000000000 ) ) ;
#4048=ORIENTED_EDGE ( 'NONE', *, *, #82, .F. ) ;
#4052=CARTESIAN_POINT ( 'NONE',  ( 0.1210307295689817542, 0.6124999999999999334, 0.03125000000000000000 ) ) ;
#4065=DIRECTION ( 'NONE',  ( 0.000000000000000000, 0.000000000000000000, -1.000000000000000000 ) ) ;
#4072=VERTEX_POINT ( 'NONE', #4941 ) ;
#4102=CARTESIAN_POINT ( 'NONE',  ( 0.000000000000000000, 0.000000000000000000, 0.000000000000000000 ) ) ;
#4119=CARTESIAN_POINT ( 'NONE',  ( -0.1250000000000000000, 0.6250000000000000000, 0.03125000000000000000 ) ) ;
#4127=EDGE_CURVE ( 'NONE', #3995, #4366, #2470, .T. ) ;
#4129=DIRECTION ( 'NONE',  ( 0.000000000000000000, 0.000000000000000000, 1.000000000000000000 ) ) ;
#4131=AXIS2_PLACEMENT_3D ( 'NONE', #5184, #7600, #4606 ) ;
#4140=FACE_OUTER_BOUND ( 'NONE', #3816, .T. ) ;
#4160=DIRECTION ( 'NONE',  ( 0.000000000000000000, 0.000000000000000000, -1.000000000000000000 ) ) ;
#4163=DIRECTION ( 'NONE',  ( 0.000000000000000000, 0.000000000000000000, 1.000000000000000000 ) ) ;
#4181=ADVANCED_FACE ( 'NONE', ( #2832 ), #5914, .T. ) ;
#4188=DIRECTION ( 'NONE',  ( 1.000000000000000000, 0.000000000000000000, 0.000000000000000000 ) ) ;
#4191=LINE ( 'NONE', #4764, #5535 ) ;
#4197=ORIENTED_EDGE ( 'NONE', *, *, #3398, .T. ) ;
#4198=CARTESIAN_POINT ( 'NONE',  ( 0.1210307295689817542, 0.6124999999999999334, -0.03125000000000000000 ) ) ;
#4220=EDGE_LOOP ( 'NONE', ( #7601, #7579 ) ) ;
#4221=DIRECTION ( 'NONE',  ( 0.000000000000000000, 1.000000000000000000, 0.000000000000000000 ) ) ;
#4232=CIRCLE ( 'NONE', #4622, 0.1100000000000000006 ) ;
#4243=EDGE_CURVE ( 'NONE', #5676, #526, #7648, .T. ) ;
#4249=EDGE_CURVE ( 'NONE', #7062, #477, #3325, .T. ) ;
#4251=CARTESIAN_POINT ( 'NONE',  ( 0.000000000000000000, 0.6124999999999999334, 0.03125000000000000000 ) ) ;
#4262=EDGE_LOOP ( 'NONE', ( #7012, #4436, #7150, #6965 ) ) ;
#4270=DIRECTION ( 'NONE',  ( 0.000000000000000000, 1.000000000000000000, 0.000000000000000000 ) ) ;
#4277=DIRECTION ( 'NONE',  ( 0.000000000000000000, 1.000000000000000000, 0.000000000000000000 ) ) ;
#4286=AXIS2_PLACEMENT_3D ( 'NONE', #1954, #3843, #726 ) ;
#4293=AXIS2_PLACEMENT_3D ( 'NONE', #4484, #1489, #6983 ) ;
#4300=DIRECTION ( 'NONE',  ( 0.000000000000000000, 1.000000000000000000, 0.000000000000000000 ) ) ;
#4302=PLANE ( 'NONE',  #7414 ) ;
#4306=LINE ( 'NONE', #8057, #2678 ) ;
#4310=CARTESIAN_POINT ( 'NONE',  ( 0.1250000000000000000, 0.6250000000000000000, -0.03125000000000000000 ) ) ;
#4311=PLANE ( 'NONE',  #203 ) ;
#4324=DIRECTION ( 'NONE',  ( 0.000000000000000000, 0.000000000000000000, 1.000000000000000000 ) ) ;
#4327=PLANE ( 'NONE',  #7558 ) ;
#4334=DIRECTION ( 'NONE',  ( -1.000000000000000000, -0.000000000000000000, -0.000000000000000000 ) ) ;
#4340=EDGE_CURVE ( 'NONE', #1116, #305, #2280, .T. ) ;
#4349=EDGE_LOOP ( 'NONE', ( #458, #3811, #5195, #1831 ) ) ;
#4356=AXIS2_PLACEMENT_3D ( 'NONE', #1095, #7364, #1055 ) ;
#4366=VERTEX_POINT ( 'NONE', #1063 ) ;
#4397=CARTESIAN_POINT ( 'NONE',  ( 0.1210307295689817680, 0.6250000000000000000, -0.03125000000000000000 ) ) ;
#4406=CIRCLE ( 'NONE', #7273, 0.1250000000000000000 ) ;
#4422=AXIS2_PLACEMENT_3D ( 'NONE', #5688, #5767, #6997 ) ;
#4426=EDGE_LOOP ( 'NONE', ( #5542, #7573 ) ) ;
#4430=ORIENTED_EDGE ( 'NONE', *, *, #2621, .T. ) ;
#4436=ORIENTED_EDGE ( 'NONE', *, *, #4733, .F. ) ;
#4443=LINE ( 'NONE', #3282, #8027 ) ;
#4450=EDGE_CURVE ( 'NONE', #526, #1756, #4306, .T. ) ;
#4457=CARTESIAN_POINT ( 'NONE',  ( 0.000000000000000000, 1.050000000000000044, -0.2112499999999999933 ) ) ;
#4460=CARTESIAN_POINT ( 'NONE',  ( 0.000000000000000000, 0.03125000000000000000, -0.1799999999999999933 ) ) ;
#4463=CARTESIAN_POINT ( 'NONE',  ( 2.778417425565558062E-17, 1.112500000000000044, -0.2112499999999999933 ) ) ;
#4480=PRODUCT_DEFINITION_FORMATION_WITH_SPECIFIED_SOURCE ( 'ANY', '', #2972, .NOT_KNOWN. ) ;
#4484=CARTESIAN_POINT ( 'NONE',  ( 0.000000000000000000, 1.112500000000000044, 0.000000000000000000 ) ) ;
#4492=CIRCLE ( 'NONE', #2792, 0.03125000000000000694 ) ;
#4496=DIRECTION ( 'NONE',  ( -0.000000000000000000, 1.000000000000000000, -0.000000000000000000 ) ) ;
#4501=VECTOR ( 'NONE', #2270, 39.37007874015748143 ) ;
#4502=AXIS2_PLACEMENT_3D ( 'NONE', #229, #1331, #7568 ) ;
#4503=ORIENTED_EDGE ( 'NONE', *, *, #5053, .F. ) ;
#4520=CIRCLE ( 'NONE', #460, 0.1100000000000000006 ) ;
#4523=ORIENTED_EDGE ( 'NONE', *, *, #1935, .F. ) ;
#4550=FACE_OUTER_BOUND ( 'NONE', #5012, .T. ) ;
#4555=AXIS2_PLACEMENT_3D ( 'NONE', #2919, #5316, #1610 ) ;
#4556=DIRECTION ( 'NONE',  ( -1.224646799147352961E-16, 0.000000000000000000, -1.000000000000000000 ) ) ;
#4564=DIRECTION ( 'NONE',  ( 0.000000000000000000, 0.000000000000000000, 1.000000000000000000 ) ) ;
#4567=FACE_OUTER_BOUND ( 'NONE', #6450, .T. ) ;
#4576=PLANE ( 'NONE',  #4422 ) ;
#4578=VERTEX_POINT ( 'NONE', #6352 ) ;
#4606=DIRECTION ( 'NONE',  ( 1.224646799147352961E-16, 0.000000000000000000, -1.000000000000000000 ) ) ;
#4607=ORIENTED_EDGE ( 'NONE', *, *, #6457, .F. ) ;
#4609=CIRCLE ( 'NONE', #2256, 0.1100000000000000006 ) ;
#4615=VERTEX_POINT ( 'NONE', #3478 ) ;
#4618=CARTESIAN_POINT ( 'NONE',  ( 2.204364238465235822E-17, 0.03125000000000000000, 0.1799999999999999933 ) ) ;
#4619=CARTESIAN_POINT ( 'NONE',  ( -0.1210307295689817542, 0.6124999999999999334, -0.03125000000000000000 ) ) ;
#4622=AXIS2_PLACEMENT_3D ( 'NONE', #2289, #492, #5452 ) ;
#4638=CARTESIAN_POINT ( 'NONE',  ( 0.000000000000000000, 0.000000000000000000, 0.000000000000000000 ) ) ;
#4641=ORIENTED_EDGE ( 'NONE', *, *, #7394, .T. ) ;
#4650=EDGE_LOOP ( 'NONE', ( #2223, #1066, #3290, #2999 ) ) ;
#4652=VECTOR ( 'NONE', #3012, 39.37007874015748143 ) ;
#4667=CYLINDRICAL_SURFACE ( 'NONE', #970, 0.1799999999999999933 ) ;
#4673=DIRECTION ( 'NONE',  ( 0.000000000000000000, 0.000000000000000000, 1.000000000000000000 ) ) ;
#4685=EDGE_CURVE ( 'NONE', #2075, #6542, #2864, .T. ) ;
#4694=ADVANCED_FACE ( 'NONE', ( #2943 ), #7784, .T. ) ;
#4716=ORIENTED_EDGE ( 'NONE', *, *, #125, .T. ) ;
#4729=ORIENTED_EDGE ( 'NONE', *, *, #6046, .T. ) ;
#4732=ORIENTED_EDGE ( 'NONE', *, *, #3601, .T. ) ;
#4733=EDGE_CURVE ( 'NONE', #6342, #6542, #1243, .T. ) ;
#4737=ADVANCED_FACE ( 'NONE', ( #66 ), #7453, .T. ) ;
#4738=EDGE_CURVE ( 'NONE', #2029, #6037, #2551, .T. ) ;
#4744=ADVANCED_FACE ( 'NONE', ( #1798 ), #1175, .F. ) ;
#4748=VECTOR ( 'NONE', #1585, 39.37007874015748143 ) ;
#4754=ORIENTED_EDGE ( 'NONE', *, *, #1273, .F. ) ;
#4757=AXIS2_PLACEMENT_3D ( 'NONE', #6350, #7492, #768 ) ;
#4764=CARTESIAN_POINT ( 'NONE',  ( 0.1250000000000000000, 0.5625000000000000000, -0.03125000000000000000 ) ) ;
#4765=AXIS2_PLACEMENT_3D ( 'NONE', #1571, #2879, #2805 ) ;
#4771=AXIS2_PLACEMENT_3D ( 'NONE', #5630, #95, #1939 ) ;
#4774=DIRECTION ( 'NONE',  ( -0.000000000000000000, -1.000000000000000000, -0.000000000000000000 ) ) ;
#4779=FACE_OUTER_BOUND ( 'NONE', #4262, .T. ) ;
#4783=CLOSED_SHELL ( 'NONE', ( #4694, #2027, #1795, #3232, #3499, #2925, #483, #4744, #2468, #3835, #1429, #3739, #5948, #939, #4181, #7147, #3201, #521, #5001, #6938, #5087, #488, #3288, #3382, #3645, #4737, #1420, #1367, #6736, #5202, #2193, #886, #5530, #2883, #1527, #2724, #6305 ) ) ;
#4791=PLANE ( 'NONE',  #4896 ) ;
#4793=EDGE_LOOP ( 'NONE', ( #5963, #5525, #6762, #3267 ) ) ;
#4795=CARTESIAN_POINT ( 'NONE',  ( 0.000000000000000000, 1.050000000000000044, 0.000000000000000000 ) ) ;
#4804=CIRCLE ( 'NONE', #1010, 0.03125000000000000694 ) ;
#4819=PLANE ( 'NONE',  #2201 ) ;
#4855=CARTESIAN_POINT ( 'NONE',  ( 0.000000000000000000, 1.425000000000000044, 0.000000000000000000 ) ) ;
#4861=DIRECTION ( 'NONE',  ( -0.000000000000000000, -1.000000000000000000, -0.000000000000000000 ) ) ;
#4873=DIRECTION ( 'NONE',  ( 0.000000000000000000, -0.000000000000000000, 1.000000000000000000 ) ) ;
#4879=CARTESIAN_POINT ( 'NONE',  ( 0.000000000000000000, 0.6250000000000000000, 0.000000000000000000 ) ) ;
#4883=PLANE ( 'NONE',  #5729 ) ;
#4884=FACE_BOUND ( 'NONE', #7863, .T. ) ;
#4887=EDGE_CURVE ( 'NONE', #1856, #2327, #6730, .T. ) ;
#4896=AXIS2_PLACEMENT_3D ( 'NONE', #2102, #7193, #887 ) ;
#4910=AXIS2_PLACEMENT_3D ( 'NONE', #4638, #3798, #6483 ) ;
#4912=AXIS2_PLACEMENT_3D ( 'NONE', #5074, #6795, #7411 ) ;
#4913=DIRECTION ( 'NONE',  ( 0.000000000000000000, 0.000000000000000000, -1.000000000000000000 ) ) ;
#4915=DIRECTION ( 'NONE',  ( 0.000000000000000000, -0.000000000000000000, 1.000000000000000000 ) ) ;
#4921=CARTESIAN_POINT ( 'NONE',  ( 0.000000000000000000, 1.425000000000000044, 0.000000000000000000 ) ) ;
#4928=VECTOR ( 'NONE', #6671, 39.37007874015748143 ) ;
#4941=CARTESIAN_POINT ( 'NONE',  ( -0.1250000000000000000, 0.5625000000000000000, -0.03125000000000000000 ) ) ;
#4943=EDGE_CURVE ( 'NONE', #7619, #6544, #1988, .T. ) ;
#4958=ORIENTED_EDGE ( 'NONE', *, *, #728, .F. ) ;
#4966=DIRECTION ( 'NONE',  ( 0.000000000000000000, 0.000000000000000000, -1.000000000000000000 ) ) ;
#4969=CARTESIAN_POINT ( 'NONE',  ( -0.1250000000000000000, 0.6250000000000000000, -0.03125000000000000000 ) ) ;
#4990=CARTESIAN_POINT ( 'NONE',  ( 0.1210307295689817680, 0.6250000000000000000, 0.03125000000000000000 ) ) ;
#5001=ADVANCED_FACE ( 'NONE', ( #5395, #2816 ), #6016, .T. ) ;
#5012=EDGE_LOOP ( 'NONE', ( #4523, #6992, #7388, #881, #6896, #5409, #3765, #2288, #3351 ) ) ;
#5022=AXIS2_PLACEMENT_3D ( 'NONE', #1953, #3880, #6382 ) ;
#5032=AXIS2_PLACEMENT_3D ( 'NONE', #847, #6993, #3182 ) ;
#5041=CYLINDRICAL_SURFACE ( 'NONE', #2963, 0.1250000000000000000 ) ;
#5048=AXIS2_PLACEMENT_3D ( 'NONE', #5687, #4300, #4913 ) ;
#5053=EDGE_CURVE ( 'NONE', #1476, #6638, #7169, .T. ) ;
#5057=CARTESIAN_POINT ( 'NONE',  ( -0.1210307295689817542, 0.6124999999999999334, 0.03125000000000000000 ) ) ;
#5058=AXIS2_PLACEMENT_3D ( 'NONE', #2175, #7709, #4673 ) ;
#5074=CARTESIAN_POINT ( 'NONE',  ( 0.000000000000000000, 1.081250000000000044, 0.000000000000000000 ) ) ;
#5080=LINE ( 'NONE', #1996, #1646 ) ;
#5086=EDGE_CURVE ( 'NONE', #1110, #2261, #6585, .T. ) ;
#5087=ADVANCED_FACE ( 'NONE', ( #4779 ), #7123, .T. ) ;
#5094=ORIENTED_EDGE ( 'NONE', *, *, #2936, .T. ) ;
#5102=EDGE_LOOP ( 'NONE', ( #3424, #4607 ) ) ;
#5104=ORIENTED_EDGE ( 'NONE', *, *, #1624, .T. ) ;
#5106=DIRECTION ( 'NONE',  ( 0.000000000000000000, 0.000000000000000000, -1.000000000000000000 ) ) ;
#5111=DIRECTION ( 'NONE',  ( -0.000000000000000000, 1.000000000000000000, -0.000000000000000000 ) ) ;
#5113=ORIENTED_EDGE ( 'NONE', *, *, #3486, .F. ) ;
#5124=VECTOR ( 'NONE', #173, 39.37007874015748143 ) ;
#5125=DIRECTION ( 'NONE',  ( -0.000000000000000000, 1.000000000000000000, -0.000000000000000000 ) ) ;
#5133=CARTESIAN_POINT ( 'NONE',  ( 0.1054677083281892608, 0.5625000000000000000, 0.03125000000000000000 ) ) ;
#5140=ORIENTED_EDGE ( 'NONE', *, *, #3231, .F. ) ;
#5141=AXIS2_PLACEMENT_3D ( 'NONE', #360, #7701, #5285 ) ;
#5147=DIRECTION ( 'NONE',  ( -0.000000000000000000, -1.000000000000000000, -0.000000000000000000 ) ) ;
#5174=DIRECTION ( 'NONE',  ( 0.000000000000000000, 0.000000000000000000, -1.000000000000000000 ) ) ;
#5184=CARTESIAN_POINT ( 'NONE',  ( 2.587066363198783776E-17, 1.081250000000000044, -0.2112499999999999933 ) ) ;
#5195=ORIENTED_EDGE ( 'NONE', *, *, #1673, .T. ) ;
#5202=ADVANCED_FACE ( 'NONE', ( #3675 ), #546, .T. ) ;
#5204=CARTESIAN_POINT ( 'NONE',  ( 0.000000000000000000, 0.000000000000000000, 0.000000000000000000 ) ) ;
#5220=CARTESIAN_POINT ( 'NONE',  ( -0.1054677083281892608, 0.6124999999999999334, -0.03125000000000000000 ) ) ;
#5225=ORIENTED_EDGE ( 'NONE', *, *, #7342, .F. ) ;
#5227=DIRECTION ( 'NONE',  ( 8.881784197001252323E-16, 0.000000000000000000, 1.000000000000000000 ) ) ;
#5228=CARTESIAN_POINT ( 'NONE',  ( 1.347111479062088626E-17, 0.000000000000000000, -0.1100000000000000006 ) ) ;
#5233=EDGE_LOOP ( 'NONE', ( #5567, #5385, #601, #5847, #5398 ) ) ;
#5244=EDGE_CURVE ( 'NONE', #3476, #7840, #6451, .T. ) ;
#5263=FACE_OUTER_BOUND ( 'NONE', #2835, .T. ) ;
#5284=ORIENTED_EDGE ( 'NONE', *, *, #679, .T. ) ;
#5285=DIRECTION ( 'NONE',  ( -1.224646799147352961E-16, 0.000000000000000000, -1.000000000000000000 ) ) ;
#5304=DIRECTION ( 'NONE',  ( 0.000000000000000000, -0.000000000000000000, 1.000000000000000000 ) ) ;
#5310=ORIENTED_EDGE ( 'NONE', *, *, #5787, .F. ) ;
#5316=DIRECTION ( 'NONE',  ( 0.000000000000000000, 1.000000000000000000, 0.000000000000000000 ) ) ;
#5318=FACE_OUTER_BOUND ( 'NONE', #5888, .T. ) ;
#5327=LINE ( 'NONE', #7814, #3453 ) ;
#5328=AXIS2_PLACEMENT_3D ( 'NONE', #1755, #6760, #6637 ) ;
#5348=EDGE_CURVE ( 'NONE', #409, #24, #1400, .T. ) ;
#5351=ORIENTED_EDGE ( 'NONE', *, *, #6513, .T. ) ;
#5356=VERTEX_POINT ( 'NONE', #5133 ) ;
#5370=ORIENTED_EDGE ( 'NONE', *, *, #2479, .T. ) ;
#5376=CARTESIAN_POINT ( 'NONE',  ( 0.000000000000000000, 0.6124999999999999334, 0.000000000000000000 ) ) ;
#5381=DIRECTION ( 'NONE',  ( 0.000000000000000000, 0.000000000000000000, -1.000000000000000000 ) ) ;
#5383=EDGE_CURVE ( 'NONE', #5676, #3956, #2717, .T. ) ;
#5385=ORIENTED_EDGE ( 'NONE', *, *, #2038, .F. ) ;
#5395=FACE_OUTER_BOUND ( 'NONE', #4426, .T. ) ;
#5396=MECHANICAL_CONTEXT ( 'NONE', #3900, 'mechanical' ) ;
#5398=ORIENTED_EDGE ( 'NONE', *, *, #7102, .F. ) ;
#5399=DIRECTION ( 'NONE',  ( -0.000000000000000000, 1.000000000000000000, -0.000000000000000000 ) ) ;
#5403=EDGE_LOOP ( 'NONE', ( #7490, #6882, #7723, #7161, #6924, #6225 ) ) ;
#5408=CARTESIAN_POINT ( 'NONE',  ( -0.1250000000000000000, 0.6250000000000000000, 0.03125000000000000000 ) ) ;
#5409=ORIENTED_EDGE ( 'NONE', *, *, #1829, .F. ) ;
#5424=CARTESIAN_POINT ( 'NONE',  ( 0.000000000000000000, 1.425000000000000044, 0.1487499999999999933 ) ) ;
#5430=AXIS2_PLACEMENT_3D ( 'NONE', #5376, #367, #1150 ) ;
#5433=CARTESIAN_POINT ( 'NONE',  ( 0.000000000000000000, 0.03125000000000000000, 0.000000000000000000 ) ) ;
#5436=DIRECTION ( 'NONE',  ( 0.000000000000000000, 1.000000000000000000, 0.000000000000000000 ) ) ;
#5448=EDGE_CURVE ( 'NONE', #7766, #2842, #2319, .T. ) ;
#5452=DIRECTION ( 'NONE',  ( 0.000000000000000000, 0.000000000000000000, 1.000000000000000000 ) ) ;
#5453=AXIS2_PLACEMENT_3D ( 'NONE', #1304, #153, #3364 ) ;
#5459=DIRECTION ( 'NONE',  ( -0.000000000000000000, -1.000000000000000000, -0.000000000000000000 ) ) ;
#5462=PRODUCT_DEFINITION_SHAPE ( 'NONE', 'NONE',  #5651 ) ;
#5479=ORIENTED_EDGE ( 'NONE', *, *, #6348, .T. ) ;
#5480=LINE ( 'NONE', #2395, #5928 ) ;
#5483=ORIENTED_EDGE ( 'NONE', *, *, #133, .F. ) ;
#5503=ORIENTED_EDGE ( 'NONE', *, *, #5086, .T. ) ;
#5525=ORIENTED_EDGE ( 'NONE', *, *, #1536, .T. ) ;
#5530=ADVANCED_FACE ( 'NONE', ( #7910 ), #4819, .T. ) ;
#5535=VECTOR ( 'NONE', #5958, 39.37007874015748143 ) ;
#5542=ORIENTED_EDGE ( 'NONE', *, *, #2736, .T. ) ;
#5551=VECTOR ( 'NONE', #4496, 39.37007874015748143 ) ;
#5560=LINE ( 'NONE', #6866, #2412 ) ;
#5567=ORIENTED_EDGE ( 'NONE', *, *, #6046, .F. ) ;
#5570=PLANE ( 'NONE',  #6365 ) ;
#5578=AXIS2_PLACEMENT_3D ( 'NONE', #3211, #6976, #5174 ) ;
#5589=CIRCLE ( 'NONE', #3362, 0.1799999999999999933 ) ;
#5600=ORIENTED_EDGE ( 'NONE', *, *, #728, .T. ) ;
#5619=DIRECTION ( 'NONE',  ( 0.000000000000000000, 1.000000000000000000, 0.000000000000000000 ) ) ;
#5628=ORIENTED_EDGE ( 'NONE', *, *, #5794, .F. ) ;
#5630=CARTESIAN_POINT ( 'NONE',  ( 0.000000000000000000, 1.362500000000000044, 0.000000000000000000 ) ) ;
#5644=ORIENTED_EDGE ( 'NONE', *, *, #4887, .F. ) ;
#5650=DIRECTION ( 'NONE',  ( -0.000000000000000000, -1.000000000000000000, -0.000000000000000000 ) ) ;
#5651=PRODUCT_DEFINITION ( 'UNKNOWN', '', #4480, #1549 ) ;
#5664=TOROIDAL_SURFACE ( 'NONE', #4356, 0.1487499999999999933, 0.03125000000000000000 ) ;
#5676=VERTEX_POINT ( 'NONE', #566 ) ;
#5687=CARTESIAN_POINT ( 'NONE',  ( 0.000000000000000000, 0.03125000000000000000, 0.000000000000000000 ) ) ;
#5688=CARTESIAN_POINT ( 'NONE',  ( -0.1250000000000000000, 0.5625000000000000000, -0.03125000000000000000 ) ) ;
#5714=DIRECTION ( 'NONE',  ( 0.000000000000000000, 0.000000000000000000, 1.000000000000000000 ) ) ;
#5720=CARTESIAN_POINT ( 'NONE',  ( 0.000000000000000000, 0.000000000000000000, 0.000000000000000000 ) ) ;
#5726=ORIENTED_EDGE ( 'NONE', *, *, #6979, .T. ) ;
#5729=AXIS2_PLACEMENT_3D ( 'NONE', #7379, #1764, #4966 ) ;
#5767=DIRECTION ( 'NONE',  ( 1.000000000000000000, 0.000000000000000000, 0.000000000000000000 ) ) ;
#5775=DIRECTION ( 'NONE',  ( 1.000000000000000000, 0.000000000000000000, 0.000000000000000000 ) ) ;
#5778=CARTESIAN_POINT ( 'NONE',  ( 0.1250000000000000000, 0.6250000000000000000, -0.03125000000000000000 ) ) ;
#5779=CARTESIAN_POINT ( 'NONE',  ( 0.000000000000000000, 0.6124999999999999334, 0.000000000000000000 ) ) ;
#5782=DIRECTION ( 'NONE',  ( 0.000000000000000000, 0.000000000000000000, 1.000000000000000000 ) ) ;
#5787=EDGE_CURVE ( 'NONE', #1684, #1575, #7303, .T. ) ;
#5794=EDGE_CURVE ( 'NONE', #6217, #6544, #896, .T. ) ;
#5809=CARTESIAN_POINT ( 'NONE',  ( -0.1210307295689817542, 0.6124999999999999334, -0.03125000000000000000 ) ) ;
#5810=DIRECTION ( 'NONE',  ( 0.000000000000000000, 0.000000000000000000, 1.000000000000000000 ) ) ;
#5817=ORIENTED_EDGE ( 'NONE', *, *, #2621, .F. ) ;
#5834=CIRCLE ( 'NONE', #864, 0.1250000000000000000 ) ;
#5847=ORIENTED_EDGE ( 'NONE', *, *, #5901, .T. ) ;
#5858=CARTESIAN_POINT ( 'NONE',  ( 0.000000000000000000, 1.425000000000000044, 0.000000000000000000 ) ) ;
#5862=AXIS2_PLACEMENT_3D ( 'NONE', #4879, #1761, #2337 ) ;
#5871=DIRECTION ( 'NONE',  ( -0.000000000000000000, -1.000000000000000000, -0.000000000000000000 ) ) ;
#5883=CYLINDRICAL_SURFACE ( 'NONE', #2200, 0.1100000000000000006 ) ;
#5884=DIRECTION ( 'NONE',  ( 0.000000000000000000, 1.000000000000000000, 0.000000000000000000 ) ) ;
#5888=EDGE_LOOP ( 'NONE', ( #7602, #5644, #589, #5113 ) ) ;
#5889=ORIENTED_EDGE ( 'NONE', *, *, #1724, .F. ) ;
#5895=EDGE_CURVE ( 'NONE', #6342, #7740, #6629, .T. ) ;
#5901=EDGE_CURVE ( 'NONE', #3971, #2487, #5080, .T. ) ;
#5902=VERTEX_POINT ( 'NONE', #697 ) ;
#5912=DIRECTION ( 'NONE',  ( -0.000000000000000000, 1.000000000000000000, -0.000000000000000000 ) ) ;
#5914=CYLINDRICAL_SURFACE ( 'NONE', #2813, 0.1799999999999999933 ) ;
#5922=( NAMED_UNIT ( * ) PLANE_ANGLE_UNIT ( ) SI_UNIT ( $, .RADIAN. ) );
#5928=VECTOR ( 'NONE', #5399, 39.37007874015748143 ) ;
#5929=EDGE_LOOP ( 'NONE', ( #5932, #6408 ) ) ;
#5932=ORIENTED_EDGE ( 'NONE', *, *, #5448, .T. ) ;
#5935=CARTESIAN_POINT ( 'NONE',  ( -0.1210307295689817680, 0.6250000000000000000, -0.03125000000000000000 ) ) ;
#5938=AXIS2_PLACEMENT_3D ( 'NONE', #2689, #3309, #7077 ) ;
#5939=CARTESIAN_POINT ( 'NONE',  ( 2.204364238465235822E-17, 0.000000000000000000, 0.1799999999999999933 ) ) ;
#5942=TOROIDAL_SURFACE ( 'NONE', #2397, 0.2112499999999999933, 0.03125000000000000000 ) ;
#5948=ADVANCED_FACE ( 'NONE', ( #4550 ), #5041, .F. ) ;
#5958=DIRECTION ( 'NONE',  ( 0.000000000000000000, 1.000000000000000000, 0.000000000000000000 ) ) ;
#5963=ORIENTED_EDGE ( 'NONE', *, *, #1273, .T. ) ;
#5967=DIRECTION ( 'NONE',  ( -0.000000000000000000, -1.000000000000000000, -0.000000000000000000 ) ) ;
#5975=CARTESIAN_POINT ( 'NONE',  ( -0.1054677083281892608, 0.000000000000000000, -0.03125000000000000000 ) ) ;
#5983=AXIS2_PLACEMENT_3D ( 'NONE', #5779, #2748, #3247 ) ;
#5991=EDGE_CURVE ( 'NONE', #7663, #3956, #344, .T. ) ;
#6016=PLANE ( 'NONE',  #7383 ) ;
#6026=DIRECTION ( 'NONE',  ( 0.000000000000000000, 0.000000000000000000, 1.000000000000000000 ) ) ;
#6034=CARTESIAN_POINT ( 'NONE',  ( 0.000000000000000000, 1.081250000000000044, 0.000000000000000000 ) ) ;
#6036=EDGE_LOOP ( 'NONE', ( #1608, #7197, #1158, #3753 ) ) ;
#6037=VERTEX_POINT ( 'NONE', #913 ) ;
#6039=DIRECTION ( 'NONE',  ( 0.000000000000000000, -1.000000000000000000, 0.000000000000000000 ) ) ;
#6046=EDGE_CURVE ( 'NONE', #2261, #1684, #2245, .T. ) ;
#6054=DIRECTION ( 'NONE',  ( -0.000000000000000000, -0.000000000000000000, -1.000000000000000000 ) ) ;
#6055=AXIS2_PLACEMENT_3D ( 'NONE', #7479, #2619, #4564 ) ;
#6062=DIRECTION ( 'NONE',  ( 0.000000000000000000, 0.000000000000000000, 1.000000000000000000 ) ) ;
#6065=EDGE_LOOP ( 'NONE', ( #1615, #3096, #1662, #535, #7222 ) ) ;
#6066=CIRCLE ( 'NONE', #5938, 0.03125000000000000694 ) ;
#6068=CARTESIAN_POINT ( 'NONE',  ( 0.000000000000000000, 1.393749999999999822, 0.1487499999999999933 ) ) ;
#6077=VECTOR ( 'NONE', #3429, 39.37007874015748143 ) ;
#6079=ORIENTED_EDGE ( 'NONE', *, *, #4887, .T. ) ;
#6099=CARTESIAN_POINT ( 'NONE',  ( -0.1250000000000000000, 0.6250000000000000000, -0.03125000000000000000 ) ) ;
#6102=AXIS2_PLACEMENT_3D ( 'NONE', #3112, #2444, #7530 ) ;
#6114=ORIENTED_EDGE ( 'NONE', *, *, #7630, .F. ) ;
#6119=DIRECTION ( 'NONE',  ( 0.000000000000000000, 0.000000000000000000, 1.000000000000000000 ) ) ;
#6124=CARTESIAN_POINT ( 'NONE',  ( 0.000000000000000000, 0.000000000000000000, 0.000000000000000000 ) ) ;
#6127=ORIENTED_EDGE ( 'NONE', *, *, #7281, .T. ) ;
#6140=DIRECTION ( 'NONE',  ( -1.000000000000000000, -0.000000000000000000, -0.000000000000000000 ) ) ;
#6154=DIMENSIONAL_EXPONENTS ( 1.000000000000000000, 0.000000000000000000, 0.000000000000000000, 0.000000000000000000, 0.000000000000000000, 0.000000000000000000, 0.000000000000000000 ) ;
#6161=FACE_BOUND ( 'NONE', #7678, .T. ) ;
#6183=DIRECTION ( 'NONE',  ( 0.000000000000000000, 0.000000000000000000, 1.000000000000000000 ) ) ;
#6184=DIRECTION ( 'NONE',  ( 0.000000000000000000, 0.000000000000000000, -1.000000000000000000 ) ) ;
#6185=DIRECTION ( 'NONE',  ( 0.000000000000000000, 1.000000000000000000, 0.000000000000000000 ) ) ;
#6187=ORIENTED_EDGE ( 'NONE', *, *, #691, .F. ) ;
#6192=EDGE_CURVE ( 'NONE', #3726, #6549, #2428, .T. ) ;
#6207=ORIENTED_EDGE ( 'NONE', *, *, #5794, .T. ) ;
#6217=VERTEX_POINT ( 'NONE', #6759 ) ;
#6220=UNCERTAINTY_MEASURE_WITH_UNIT (LENGTH_MEASURE( 1.000000000000000082E-05 ), #2225, 'distance_accuracy_value', 'NONE');
#6225=ORIENTED_EDGE ( 'NONE', *, *, #7394, .F. ) ;
#6235=FACE_OUTER_BOUND ( 'NONE', #840, .T. ) ;
#6247=FACE_OUTER_BOUND ( 'NONE', #2203, .T. ) ;
#6256=CARTESIAN_POINT ( 'NONE',  ( 0.000000000000000000, 0.000000000000000000, 0.000000000000000000 ) ) ;
#6260=VECTOR ( 'NONE', #6770, 39.37007874015748143 ) ;
#6264=CARTESIAN_POINT ( 'NONE',  ( 0.000000000000000000, 0.6250000000000000000, 0.000000000000000000 ) ) ;
#6296=CARTESIAN_POINT ( 'NONE',  ( -0.1250000000000000000, 0.5625000000000000000, 0.03125000000000000000 ) ) ;
#6305=ADVANCED_FACE ( 'NONE', ( #6420 ), #4576, .T. ) ;
#6306=CARTESIAN_POINT ( 'NONE',  ( 0.000000000000000000, 0.000000000000000000, 0.000000000000000000 ) ) ;
#6307=EDGE_LOOP ( 'NONE', ( #4732, #3111, #2485, #7881, #2804, #4006 ) ) ;
#6311=VERTEX_POINT ( 'NONE', #5809 ) ;
#6328=EDGE_CURVE ( 'NONE', #5902, #1252, #484, .T. ) ;
#6340=MANIFOLD_SOLID_BREP ( 'Cut-Extrude5', #4783 ) ;
#6342=VERTEX_POINT ( 'NONE', #4460 ) ;
#6348=EDGE_CURVE ( 'NONE', #7740, #2606, #2052, .T. ) ;
#6350=CARTESIAN_POINT ( 'NONE',  ( -0.1250000000000000000, 0.5625000000000000000, 0.03125000000000000000 ) ) ;
#6352=CARTESIAN_POINT ( 'NONE',  ( 2.013013176098461537E-17, 1.425000000000000044, -0.1487499999999999933 ) ) ;
#6362=CYLINDRICAL_SURFACE ( 'NONE', #3987, 0.1100000000000000006 ) ;
#6363=DIRECTION ( 'NONE',  ( 0.000000000000000000, 1.000000000000000000, 0.000000000000000000 ) ) ;
#6365=AXIS2_PLACEMENT_3D ( 'NONE', #5408, #7369, #3686 ) ;
#6375=AXIS2_PLACEMENT_3D ( 'NONE', #6264, #4861, #4324 ) ;
#6382=DIRECTION ( 'NONE',  ( 0.000000000000000000, 0.000000000000000000, 1.000000000000000000 ) ) ;
#6386=PLANE ( 'NONE',  #4757 ) ;
#6391=EDGE_CURVE ( 'NONE', #7457, #6217, #186, .T. ) ;
#6395=DIRECTION ( 'NONE',  ( 1.000000000000000000, 0.000000000000000000, -1.224646799147353207E-16 ) ) ;
#6405=DIRECTION ( 'NONE',  ( 0.000000000000000000, 0.000000000000000000, 1.000000000000000000 ) ) ;
#6408=ORIENTED_EDGE ( 'NONE', *, *, #1924, .T. ) ;
#6414=CARTESIAN_POINT ( 'NONE',  ( -0.1250000000000000000, 0.6250000000000000000, -0.03125000000000000000 ) ) ;
#6420=FACE_OUTER_BOUND ( 'NONE', #6065, .T. ) ;
#6427=DIRECTION ( 'NONE',  ( 0.000000000000000000, 0.000000000000000000, 1.000000000000000000 ) ) ;
#6434=EDGE_CURVE ( 'NONE', #2029, #7766, #3106, .T. ) ;
#6450=EDGE_LOOP ( 'NONE', ( #3095, #1042, #264, #6207 ) ) ;
#6451=LINE ( 'NONE', #791, #3063 ) ;
#6453=CARTESIAN_POINT ( 'NONE',  ( 0.000000000000000000, 0.6250000000000000000, 0.000000000000000000 ) ) ;
#6457=EDGE_CURVE ( 'NONE', #7619, #7457, #7675, .T. ) ;
#6480=ORIENTED_EDGE ( 'NONE', *, *, #1330, .F. ) ;
#6483=DIRECTION ( 'NONE',  ( 0.000000000000000000, 0.000000000000000000, 1.000000000000000000 ) ) ;
#6484=DIRECTION ( 'NONE',  ( -0.000000000000000000, -1.000000000000000000, -0.000000000000000000 ) ) ;
#6490=LINE ( 'NONE', #876, #7275 ) ;
#6513=EDGE_CURVE ( 'NONE', #7994, #7663, #2817, .T. ) ;
#6542=VERTEX_POINT ( 'NONE', #4618 ) ;
#6544=VERTEX_POINT ( 'NONE', #908 ) ;
#6549=VERTEX_POINT ( 'NONE', #3400 ) ;
#6561=CARTESIAN_POINT ( 'NONE',  ( 0.1250000000000000000, 0.6250000000000000000, -0.03125000000000000000 ) ) ;
#6566=APPLICATION_CONTEXT ( 'configuration controlled 3d designs of mechanical parts and assemblies' ) ;
#6572=EDGE_LOOP ( 'NONE', ( #6713, #7529, #7765, #1998 ) ) ;
#6574=VERTEX_POINT ( 'NONE', #5935 ) ;
#6575=LENGTH_MEASURE_WITH_UNIT ( LENGTH_MEASURE( 0.02539999999999999897 ), #2194 );
#6580=FACE_OUTER_BOUND ( 'NONE', #3116, .T. ) ;
#6581=VECTOR ( 'NONE', #727, 39.37007874015748143 ) ;
#6585=LINE ( 'NONE', #7878, #4501 ) ;
#6597=AXIS2_PLACEMENT_3D ( 'NONE', #3538, #217, #5227 ) ;
#6600=EDGE_CURVE ( 'NONE', #1252, #353, #3592, .T. ) ;
#6613=AXIS2_PLACEMENT_3D ( 'NONE', #7239, #5436, #7083 ) ;
#6629=CIRCLE ( 'NONE', #1916, 0.03125000000000000694 ) ;
#6637=DIRECTION ( 'NONE',  ( -1.000000000000000000, 0.000000000000000000, -0.000000000000000000 ) ) ;
#6638=VERTEX_POINT ( 'NONE', #513 ) ;
#6641=VECTOR ( 'NONE', #6701, 39.37007874015748143 ) ;
#6643=AXIS2_PLACEMENT_3D ( 'NONE', #2580, #3367, #198 ) ;
#6667=FACE_OUTER_BOUND ( 'NONE', #1402, .T. ) ;
#6671=DIRECTION ( 'NONE',  ( 0.000000000000000000, 0.000000000000000000, 1.000000000000000000 ) ) ;
#6691=CARTESIAN_POINT ( 'NONE',  ( -0.1210307295689817542, 0.6124999999999999334, 0.03125000000000000000 ) ) ;
#6701=DIRECTION ( 'NONE',  ( -1.000000000000000000, 0.000000000000000000, 0.000000000000000000 ) ) ;
#6702=DIRECTION ( 'NONE',  ( 0.000000000000000000, 1.000000000000000000, 0.000000000000000000 ) ) ;
#6713=ORIENTED_EDGE ( 'NONE', *, *, #4685, .F. ) ;
#6718=ORIENTED_EDGE ( 'NONE', *, *, #1724, .T. ) ;
#6719=AXIS2_PLACEMENT_3D ( 'NONE', #7253, #1028, #1560 ) ;
#6722=TOROIDAL_SURFACE ( 'NONE', #7115, 0.1487499999999999933, 0.03125000000000000000 ) ;
#6730=CIRCLE ( 'NONE', #5022, 0.1799999999999999933 ) ;
#6736=ADVANCED_FACE ( 'NONE', ( #3545 ), #4327, .F. ) ;
#6737=DIRECTION ( 'NONE',  ( 0.000000000000000000, 0.000000000000000000, 1.000000000000000000 ) ) ;
#6757=AXIS2_PLACEMENT_3D ( 'NONE', #1036, #4037, #5304 ) ;
#6759=CARTESIAN_POINT ( 'NONE',  ( 0.000000000000000000, 1.425000000000000044, 0.1100000000000000006 ) ) ;
#6760=DIRECTION ( 'NONE',  ( 0.000000000000000000, 0.000000000000000000, -1.000000000000000000 ) ) ;
#6762=ORIENTED_EDGE ( 'NONE', *, *, #7735, .F. ) ;
#6770=DIRECTION ( 'NONE',  ( 0.000000000000000000, 0.000000000000000000, 1.000000000000000000 ) ) ;
#6775=ORIENTED_EDGE ( 'NONE', *, *, #7844, .F. ) ;
#6781=ORIENTED_EDGE ( 'NONE', *, *, #7102, .T. ) ;
#6795=DIRECTION ( 'NONE',  ( 0.000000000000000000, 1.000000000000000000, 0.000000000000000000 ) ) ;
#6810=DIRECTION ( 'NONE',  ( 0.000000000000000000, -0.000000000000000000, 1.000000000000000000 ) ) ;
#6820=DIRECTION ( 'NONE',  ( 1.000000000000000000, 0.000000000000000000, -0.000000000000000000 ) ) ;
#6832=CARTESIAN_POINT ( 'NONE',  ( 0.000000000000000000, 1.050000000000000044, -0.1799999999999999933 ) ) ;
#6846=VECTOR ( 'NONE', #366, 39.37007874015748143 ) ;
#6866=CARTESIAN_POINT ( 'NONE',  ( -0.1250000000000000000, 0.6250000000000000000, 0.03125000000000000000 ) ) ;
#6882=ORIENTED_EDGE ( 'NONE', *, *, #5244, .T. ) ;
#6883=DIRECTION ( 'NONE',  ( -0.000000000000000000, 1.000000000000000000, -0.000000000000000000 ) ) ;
#6892=CARTESIAN_POINT ( 'NONE',  ( 0.000000000000000000, 0.5625000000000000000, 0.000000000000000000 ) ) ;
#6896=ORIENTED_EDGE ( 'NONE', *, *, #5787, .T. ) ;
#6910=CARTESIAN_POINT ( 'NONE',  ( -0.1054677083281892608, 0.5625000000000000000, -0.03125000000000000000 ) ) ;
#6911=AXIS2_PLACEMENT_3D ( 'NONE', #7580, #7009, #119 ) ;
#6916=ORIENTED_EDGE ( 'NONE', *, *, #7844, .T. ) ;
#6924=ORIENTED_EDGE ( 'NONE', *, *, #3395, .T. ) ;
#6937=DIRECTION ( 'NONE',  ( -0.000000000000000000, -1.000000000000000000, -0.000000000000000000 ) ) ;
#6938=ADVANCED_FACE ( 'NONE', ( #4567 ), #5883, .F. ) ;
#6944=ORIENTED_EDGE ( 'NONE', *, *, #522, .F. ) ;
#6945=EDGE_CURVE ( 'NONE', #1252, #6574, #3500, .T. ) ;
#6965=ORIENTED_EDGE ( 'NONE', *, *, #7796, .F. ) ;
#6976=DIRECTION ( 'NONE',  ( 0.000000000000000000, 1.000000000000000000, 0.000000000000000000 ) ) ;
#6979=EDGE_CURVE ( 'NONE', #6311, #7663, #836, .T. ) ;
#6981=DIRECTION ( 'NONE',  ( 0.000000000000000000, 0.000000000000000000, 1.000000000000000000 ) ) ;
#6983=DIRECTION ( 'NONE',  ( 0.000000000000000000, 0.000000000000000000, -1.000000000000000000 ) ) ;
#6992=ORIENTED_EDGE ( 'NONE', *, *, #4340, .F. ) ;
#6993=DIRECTION ( 'NONE',  ( -0.000000000000000000, -1.000000000000000000, -0.000000000000000000 ) ) ;
#6997=DIRECTION ( 'NONE',  ( 0.000000000000000000, 0.000000000000000000, -1.000000000000000000 ) ) ;
#7009=DIRECTION ( 'NONE',  ( -0.000000000000000000, -1.000000000000000000, -0.000000000000000000 ) ) ;
#7011=CIRCLE ( 'NONE', #4131, 0.03125000000000000694 ) ;
#7012=ORIENTED_EDGE ( 'NONE', *, *, #2936, .F. ) ;
#7015=DIRECTION ( 'NONE',  ( 0.000000000000000000, 0.000000000000000000, -1.000000000000000000 ) ) ;
#7035=ORIENTED_EDGE ( 'NONE', *, *, #1536, .F. ) ;
#7040=DIRECTION ( 'NONE',  ( 0.000000000000000000, 0.000000000000000000, 1.000000000000000000 ) ) ;
#7062=VERTEX_POINT ( 'NONE', #3617 ) ;
#7070=EDGE_LOOP ( 'NONE', ( #2962, #2097, #3749, #5140, #3392, #2762, #5483, #6944 ) ) ;
#7077=DIRECTION ( 'NONE',  ( 1.224646799147352961E-16, 0.000000000000000000, -1.000000000000000000 ) ) ;
#7083=DIRECTION ( 'NONE',  ( 0.000000000000000000, 0.000000000000000000, 1.000000000000000000 ) ) ;
#7102=EDGE_CURVE ( 'NONE', #1684, #2487, #7981, .T. ) ;
#7105=ORIENTED_EDGE ( 'NONE', *, *, #6328, .T. ) ;
#7107=DIRECTION ( 'NONE',  ( 1.000000000000000000, 0.000000000000000000, 0.000000000000000000 ) ) ;
#7109=CARTESIAN_POINT ( 'NONE',  ( 1.530808498934191201E-17, 0.6124999999999999334, -0.1250000000000000000 ) ) ;
#7114=EDGE_LOOP ( 'NONE', ( #5479, #3337 ) ) ;
#7115=AXIS2_PLACEMENT_3D ( 'NONE', #257, #347, #4160 ) ;
#7118=CYLINDRICAL_SURFACE ( 'NONE', #7640, 0.1100000000000000006 ) ;
#7119=ORIENTED_EDGE ( 'NONE', *, *, #2612, .F. ) ;
#7123=TOROIDAL_SURFACE ( 'NONE', #3584, 0.1487499999999999933, 0.03125000000000000000 ) ;
#7141=VERTEX_POINT ( 'NONE', #533 ) ;
#7147=ADVANCED_FACE ( 'NONE', ( #1154, #6161 ), #4883, .T. ) ;
#7150=ORIENTED_EDGE ( 'NONE', *, *, #5895, .T. ) ;
#7161=ORIENTED_EDGE ( 'NONE', *, *, #5086, .F. ) ;
#7169=LINE ( 'NONE', #3515, #6077 ) ;
#7179=CARTESIAN_POINT ( 'NONE',  ( -0.1250000000000000000, 0.5625000000000000000, -0.03125000000000000000 ) ) ;
#7193=DIRECTION ( 'NONE',  ( 0.000000000000000000, 1.000000000000000000, 0.000000000000000000 ) ) ;
#7197=ORIENTED_EDGE ( 'NONE', *, *, #1223, .T. ) ;
#7222=ORIENTED_EDGE ( 'NONE', *, *, #6600, .F. ) ;
#7223=FACE_OUTER_BOUND ( 'NONE', #7767, .T. ) ;
#7236=CIRCLE ( 'NONE', #3567, 0.1100000000000000006 ) ;
#7238=DIRECTION ( 'NONE',  ( -0.000000000000000000, 1.000000000000000000, -0.000000000000000000 ) ) ;
#7239=CARTESIAN_POINT ( 'NONE',  ( 0.000000000000000000, 1.362500000000000044, 0.000000000000000000 ) ) ;
#7242=CARTESIAN_POINT ( 'NONE',  ( 0.1054677083281892608, 0.6124999999999999334, -0.03125000000000000000 ) ) ;
#7244=CIRCLE ( 'NONE', #6719, 0.1799999999999999933 ) ;
#7253=CARTESIAN_POINT ( 'NONE',  ( 0.000000000000000000, 0.03125000000000000000, 0.000000000000000000 ) ) ;
#7255=CIRCLE ( 'NONE', #5032, 0.1100000000000000006 ) ;
#7272=DIRECTION ( 'NONE',  ( 0.000000000000000000, 0.000000000000000000, -1.000000000000000000 ) ) ;
#7273=AXIS2_PLACEMENT_3D ( 'NONE', #47, #7589, #6405 ) ;
#7275=VECTOR ( 'NONE', #2221, 39.37007874015748143 ) ;
#7281=EDGE_CURVE ( 'NONE', #1555, #2075, #1276, .T. ) ;
#7285=CARTESIAN_POINT ( 'NONE',  ( 2.204364238465235822E-17, 1.393749999999999822, 0.1799999999999999933 ) ) ;
#7294=FACE_OUTER_BOUND ( 'NONE', #6307, .T. ) ;
#7303=CIRCLE ( 'NONE', #5862, 0.1250000000000000000 ) ;
#7315=DIRECTION ( 'NONE',  ( 1.000000000000000000, 0.000000000000000000, -0.000000000000000000 ) ) ;
#7323=CARTESIAN_POINT ( 'NONE',  ( 0.000000000000000000, 1.112500000000000044, -0.1799999999999999933 ) ) ;
#7342=EDGE_CURVE ( 'NONE', #6549, #3726, #2326, .T. ) ;
#7346=DIRECTION ( 'NONE',  ( 0.000000000000000000, 1.000000000000000000, 0.000000000000000000 ) ) ;
#7358=DIRECTION ( 'NONE',  ( 0.000000000000000000, 0.000000000000000000, 1.000000000000000000 ) ) ;
#7360=CARTESIAN_POINT ( 'NONE',  ( -0.1250000000000000000, 0.6250000000000000000, 0.03125000000000000000 ) ) ;
#7364=DIRECTION ( 'NONE',  ( 0.000000000000000000, 1.000000000000000000, 0.000000000000000000 ) ) ;
#7369=DIRECTION ( 'NONE',  ( 0.000000000000000000, 1.000000000000000000, 0.000000000000000000 ) ) ;
#7372=ORIENTED_EDGE ( 'NONE', *, *, #3231, .T. ) ;
#7379=CARTESIAN_POINT ( 'NONE',  ( -1.256933281983527929E-15, 1.050000000000000044, 0.1799999999999999933 ) ) ;
#7383=AXIS2_PLACEMENT_3D ( 'NONE', #2162, #6702, #1582 ) ;
#7388=ORIENTED_EDGE ( 'NONE', *, *, #3395, .F. ) ;
#7394=EDGE_CURVE ( 'NONE', #2990, #1116, #3817, .T. ) ;
#7405=CARTESIAN_POINT ( 'NONE',  ( 0.1054677083281892608, 0.000000000000000000, -0.03125000000000000000 ) ) ;
#7411=DIRECTION ( 'NONE',  ( 0.000000000000000000, 0.000000000000000000, -1.000000000000000000 ) ) ;
#7414=AXIS2_PLACEMENT_3D ( 'NONE', #2899, #6185, #4915 ) ;
#7425=AXIS2_PLACEMENT_3D ( 'NONE', #1373, #1335, #687 ) ;
#7453=PLANE ( 'NONE',  #6102 ) ;
#7457=VERTEX_POINT ( 'NONE', #1119 ) ;
#7479=CARTESIAN_POINT ( 'NONE',  ( 0.000000000000000000, 1.112500000000000044, 0.000000000000000000 ) ) ;
#7490=ORIENTED_EDGE ( 'NONE', *, *, #133, .T. ) ;
#7492=DIRECTION ( 'NONE',  ( 0.000000000000000000, 0.000000000000000000, -1.000000000000000000 ) ) ;
#7504=ORIENTED_EDGE ( 'NONE', *, *, #1236, .T. ) ;
#7527=EDGE_CURVE ( 'NONE', #353, #6574, #2498, .T. ) ;
#7529=ORIENTED_EDGE ( 'NONE', *, *, #7630, .T. ) ;
#7530=DIRECTION ( 'NONE',  ( 0.000000000000000000, 0.000000000000000000, 1.000000000000000000 ) ) ;
#7534=DIRECTION ( 'NONE',  ( 0.000000000000000000, 0.000000000000000000, 1.000000000000000000 ) ) ;
#7545=DIRECTION ( 'NONE',  ( 0.000000000000000000, 0.000000000000000000, 1.000000000000000000 ) ) ;
#7558=AXIS2_PLACEMENT_3D ( 'NONE', #7360, #594, #2318 ) ;
#7568=DIRECTION ( 'NONE',  ( 0.000000000000000000, -0.000000000000000000, 1.000000000000000000 ) ) ;
#7573=ORIENTED_EDGE ( 'NONE', *, *, #3486, .T. ) ;
#7579=ORIENTED_EDGE ( 'NONE', *, *, #5348, .T. ) ;
#7580=CARTESIAN_POINT ( 'NONE',  ( 0.000000000000000000, 1.050000000000000044, 0.000000000000000000 ) ) ;
#7589=DIRECTION ( 'NONE',  ( 0.000000000000000000, 1.000000000000000000, 0.000000000000000000 ) ) ;
#7600=DIRECTION ( 'NONE',  ( 1.000000000000000000, -0.000000000000000000, 1.224646799147353207E-16 ) ) ;
#7601=ORIENTED_EDGE ( 'NONE', *, *, #7735, .T. ) ;
#7602=ORIENTED_EDGE ( 'NONE', *, *, #2887, .F. ) ;
#7614=CARTESIAN_POINT ( 'NONE',  ( 0.000000000000000000, 0.6124999999999999334, -0.03125000000000000000 ) ) ;
#7619=VERTEX_POINT ( 'NONE', #790 ) ;
#7630=EDGE_CURVE ( 'NONE', #2075, #1555, #5589, .T. ) ;
#7640=AXIS2_PLACEMENT_3D ( 'NONE', #6306, #3262, #2074 ) ;
#7644=ORIENTED_EDGE ( 'NONE', *, *, #7342, .T. ) ;
#7646=CARTESIAN_POINT ( 'NONE',  ( 0.000000000000000000, 1.362500000000000044, 0.000000000000000000 ) ) ;
#7648=CIRCLE ( 'NONE', #4910, 0.1100000000000000006 ) ;
#7663=VERTEX_POINT ( 'NONE', #5220 ) ;
#7674=VECTOR ( 'NONE', #2745, 39.37007874015748143 ) ;
#7675=CIRCLE ( 'NONE', #1142, 0.1100000000000000006 ) ;
#7676=VECTOR ( 'NONE', #3664, 39.37007874015748143 ) ;
#7678=EDGE_LOOP ( 'NONE', ( #2709, #6114 ) ) ;
#7699=EDGE_CURVE ( 'NONE', #305, #6311, #1390, .T. ) ;
#7701=DIRECTION ( 'NONE',  ( 1.000000000000000000, 0.000000000000000000, -1.224646799147353207E-16 ) ) ;
#7709=DIRECTION ( 'NONE',  ( -0.000000000000000000, -1.000000000000000000, -0.000000000000000000 ) ) ;
#7718=DIRECTION ( 'NONE',  ( -0.000000000000000000, 1.000000000000000000, -0.000000000000000000 ) ) ;
#7723=ORIENTED_EDGE ( 'NONE', *, *, #2038, .T. ) ;
#7728=LINE ( 'NONE', #4619, #4748 ) ;
#7735=EDGE_CURVE ( 'NONE', #24, #409, #2964, .T. ) ;
#7740=VERTEX_POINT ( 'NONE', #1393 ) ;
#7750=AXIS2_PLACEMENT_3D ( 'NONE', #489, #7971, #4873 ) ;
#7758=LINE ( 'NONE', #2848, #43 ) ;
#7765=ORIENTED_EDGE ( 'NONE', *, *, #3028, .T. ) ;
#7766=VERTEX_POINT ( 'NONE', #165 ) ;
#7767=EDGE_LOOP ( 'NONE', ( #2784, #5094, #129, #1121 ) ) ;
#7773=AXIS2_PLACEMENT_3D ( 'NONE', #4855, #7346, #6737 ) ;
#7775=ORIENTED_EDGE ( 'NONE', *, *, #2736, .F. ) ;
#7784=TOROIDAL_SURFACE ( 'NONE', #3078, 0.2112499999999999933, 0.03125000000000000000 ) ;
#7796=EDGE_CURVE ( 'NONE', #2606, #7740, #612, .T. ) ;
#7814=CARTESIAN_POINT ( 'NONE',  ( 0.000000000000000000, 0.000000000000000000, -0.1799999999999999933 ) ) ;
#7817=DIRECTION ( 'NONE',  ( -0.000000000000000000, -1.000000000000000000, -0.000000000000000000 ) ) ;
#7820=EDGE_LOOP ( 'NONE', ( #2072, #3558, #3199, #7372, #3299, #6916 ) ) ;
#7821=CYLINDRICAL_SURFACE ( 'NONE', #1737, 0.1100000000000000006 ) ;
#7829=ORIENTED_EDGE ( 'NONE', *, *, #5991, .F. ) ;
#7836=DIRECTION ( 'NONE',  ( 0.000000000000000000, 0.000000000000000000, -1.000000000000000000 ) ) ;
#7840=VERTEX_POINT ( 'NONE', #2974 ) ;
#7844=EDGE_CURVE ( 'NONE', #1913, #661, #1782, .T. ) ;
#7853=CARTESIAN_POINT ( 'NONE',  ( -0.1250000000000000000, 0.5625000000000000000, -0.03125000000000000000 ) ) ;
#7863=EDGE_LOOP ( 'NONE', ( #5370, #3334 ) ) ;
#7869=FACE_OUTER_BOUND ( 'NONE', #953, .T. ) ;
#7870=ORIENTED_EDGE ( 'NONE', *, *, #1184, .F. ) ;
#7871=CIRCLE ( 'NONE', #685, 0.03125000000000000694 ) ;
#7878=CARTESIAN_POINT ( 'NONE',  ( -0.1250000000000000000, 0.6250000000000000000, -0.03125000000000000000 ) ) ;
#7881=ORIENTED_EDGE ( 'NONE', *, *, #125, .F. ) ;
#7891=TOROIDAL_SURFACE ( 'NONE', #4765, 0.2112499999999999933, 0.03125000000000000000 ) ;
#7892=CARTESIAN_POINT ( 'NONE',  ( 0.1250000000000000000, 0.5625000000000000000, -0.03125000000000000000 ) ) ;
#7894=DIRECTION ( 'NONE',  ( 0.000000000000000000, -0.000000000000000000, 1.000000000000000000 ) ) ;
#7909=DIRECTION ( 'NONE',  ( 0.000000000000000000, 0.000000000000000000, 1.000000000000000000 ) ) ;
#7910=FACE_OUTER_BOUND ( 'NONE', #2900, .T. ) ;
#7916=AXIS2_PLACEMENT_3D ( 'NONE', #750, #6937, #5782 ) ;
#7922=CARTESIAN_POINT ( 'NONE',  ( 0.000000000000000000, 0.000000000000000000, -0.1799999999999999933 ) ) ;
#7926=EDGE_CURVE ( 'NONE', #1110, #1684, #1661, .T. ) ;
#7939=ORIENTED_EDGE ( 'NONE', *, *, #3398, .F. ) ;
#7941=DIRECTION ( 'NONE',  ( -1.000000000000000000, 0.000000000000000000, 0.000000000000000000 ) ) ;
#7950=CARTESIAN_POINT ( 'NONE',  ( -0.1250000000000000000, 0.5625000000000000000, 0.03125000000000000000 ) ) ;
#7971=DIRECTION ( 'NONE',  ( 0.000000000000000000, 1.000000000000000000, 0.000000000000000000 ) ) ;
#7972=ORIENTED_EDGE ( 'NONE', *, *, #5383, .T. ) ;
#7981=LINE ( 'NONE', #4310, #6260 ) ;
#7985=EDGE_CURVE ( 'NONE', #477, #1252, #2018, .T. ) ;
#7994=VERTEX_POINT ( 'NONE', #6910 ) ;
#7995=ORIENTED_EDGE ( 'NONE', *, *, #1236, .F. ) ;
#8012=FACE_OUTER_BOUND ( 'NONE', #3909, .T. ) ;
#8027=VECTOR ( 'NONE', #128, 39.37007874015748143 ) ;
#8044=TOROIDAL_SURFACE ( 'NONE', #3610, 0.1487499999999999933, 0.03125000000000000000 ) ;
#8057=CARTESIAN_POINT ( 'NONE',  ( 0.000000000000000000, 0.000000000000000000, 0.1100000000000000006 ) ) ;
#8082=CARTESIAN_POINT ( 'NONE',  ( -0.1250000000000000000, 0.5625000000000000000, -0.03125000000000000000 ) ) ;
#8101=COLOUR_RGB('Deep Blue', 0.66274510, 0.83137255, 0.94901961);
#8102=FILL_AREA_STYLE_COLOUR('',#8101);
#8103=FILL_AREA_STYLE('',(#8102));
#8104=SURFACE_STYLE_FILL_AREA(#8103);
#8105=SURFACE_SIDE_STYLE('',(#8104));
#8106=SURFACE_STYLE_USAGE(.BOTH.,#8105);
#8107=PRESENTATION_STYLE_ASSIGNMENT((#8106));
#8148=STYLED_ITEM('',(#8107),#6340);
#8149=MECHANICAL_DESIGN_GEOMETRIC_PRESENTATION_REPRESENTATION('',(#8148),#1726);
ENDSEC;
END-ISO-10303-21;
